ISO-10303-21;
HEADER;
/* Generated by software containing ST-Developer
 * from STEP Tools, Inc. (www.steptools.com) 
 */

FILE_DESCRIPTION(
/* description */ (''),
/* implementation_level */ '2;1');

FILE_NAME(
/* name */ '03_Lug_Nut_1-2-20_60deg_Cone.step',
/* time_stamp */ '2026-10-25T01:26:34-07:00',
/* author */ (''),
/* organization */ (''),
/* preprocessor_version */ 'ST-DEVELOPER v20.2',
/* originating_system */ 'Autodesk Translation Framework v15.15.0.0',
/* authorisation */ '');

FILE_SCHEMA (('AUTOMOTIVE_DESIGN { 1 0 10303 214 3 1 1 }'));
ENDSEC;

DATA;
#10=MECHANICAL_DESIGN_GEOMETRIC_PRESENTATION_REPRESENTATION('',(#333),#71628);
#289=B_SPLINE_SURFACE_WITH_KNOTS('',3,3,((#71137,#71138,#71139,#71140,#71141,
#71142),(#71143,#71144,#71145,#71146,#71147,#71148),(#71149,#71150,#71151,
#71152,#71153,#71154),(#71155,#71156,#71157,#71158,#71159,#71160)),
 .UNSPECIFIED.,.F.,.F.,.F.,(4,4),(4,1,1,4),(0.,1.),(0.111993552465714,0.578527205932438,
0.889549641576921,1.2005720772214),.UNSPECIFIED.);
#290=B_SPLINE_SURFACE_WITH_KNOTS('',3,3,((#71191,#71192,#71193,#71194,#71195,
#71196),(#71197,#71198,#71199,#71200,#71201,#71202),(#71203,#71204,#71205,
#71206,#71207,#71208),(#71209,#71210,#71211,#71212,#71213,#71214)),
 .UNSPECIFIED.,.F.,.F.,.F.,(4,4),(4,1,1,4),(0.,1.),(0.111993552465714,0.578527205932438,
0.889549641576921,1.2005720772214),.UNSPECIFIED.);
#291=B_SPLINE_SURFACE_WITH_KNOTS('',3,3,((#71285,#71286,#71287,#71288,#71289,
#71290),(#71291,#71292,#71293,#71294,#71295,#71296),(#71297,#71298,#71299,
#71300,#71301,#71302),(#71303,#71304,#71305,#71306,#71307,#71308)),
 .UNSPECIFIED.,.F.,.F.,.F.,(4,4),(4,1,1,4),(0.,1.),(0.111993552465713,0.423015988110196,
0.734038423754679,1.2005720772214),.UNSPECIFIED.);
#292=B_SPLINE_SURFACE_WITH_KNOTS('',3,3,((#71437,#71438,#71439,#71440,#71441,
#71442),(#71443,#71444,#71445,#71446,#71447,#71448),(#71449,#71450,#71451,
#71452,#71453,#71454),(#71455,#71456,#71457,#71458,#71459,#71460)),
 .UNSPECIFIED.,.F.,.F.,.F.,(4,4),(4,1,1,4),(0.,1.),(0.111993552465714,0.423015988110197,
0.73403842375468,1.2005720772214),.UNSPECIFIED.);
#293=B_SPLINE_SURFACE_WITH_KNOTS('',3,3,((#71470,#71471,#71472,#71473,#71474,
#71475),(#71476,#71477,#71478,#71479,#71480,#71481),(#71482,#71483,#71484,
#71485,#71486,#71487),(#71488,#71489,#71490,#71491,#71492,#71493)),
 .UNSPECIFIED.,.F.,.F.,.F.,(4,4),(4,1,1,4),(0.,1.),(0.111993552465714,0.578527205932439,
0.889549641576922,1.20057207722141),.UNSPECIFIED.);
#294=B_SPLINE_SURFACE_WITH_KNOTS('',3,3,((#71506,#71507,#71508,#71509,#71510,
#71511),(#71512,#71513,#71514,#71515,#71516,#71517),(#71518,#71519,#71520,
#71521,#71522,#71523),(#71524,#71525,#71526,#71527,#71528,#71529)),
 .UNSPECIFIED.,.F.,.F.,.F.,(4,4),(4,1,1,4),(0.,1.),(0.111993552465714,0.578527205932438,
0.889549641576921,1.2005720772214),.UNSPECIFIED.);
#307=SHAPE_REPRESENTATION_RELATIONSHIP('SRR','None',#71695,#320);
#320=ADVANCED_BREP_SHAPE_REPRESENTATION('',(#346),#71627);
#333=STYLED_ITEM('',(#71825),#346);
#346=MANIFOLD_SOLID_BREP('Body1',#34220);
#805=B_SPLINE_CURVE_WITH_KNOTS('',3,(#70885,#70886,#70887,#70888,#70889,
#70890,#70891,#70892,#70893,#70894,#70895,#70896,#70897,#70898,#70899,#70900,
#70901,#70902,#70903),.UNSPECIFIED.,.F.,.F.,(4,3,3,3,3,3,4),(-0.229761503419508,
-0.206166571473124,-0.159724811114511,-0.12550437800065,-0.0807834581112385,
-0.0377756277020877,0.),.UNSPECIFIED.);
#806=B_SPLINE_CURVE_WITH_KNOTS('',3,(#70907,#70908,#70909,#70910,#70911,
#70912,#70913,#70914,#70915,#70916,#70917,#70918,#70919,#70920,#70921,#70922,
#70923,#70924,#70925,#70926,#70927,#70928,#70929,#70930,#70931,#70932,#70933,
#70934,#70935,#70936,#70937,#70938,#70939,#70940,#70941,#70942,#70943),
 .UNSPECIFIED.,.F.,.F.,(4,3,3,3,3,3,3,3,3,3,3,3,4),(-0.459480514361734,
-0.443345601466461,-0.398418086430754,-0.369143093793813,-0.320534667577263,
-0.278580845736582,-0.221174845679046,-0.206166571473069,-0.159724811114448,
-0.125504378000605,-0.0807878344312463,-0.037784169760125,0.),
 .UNSPECIFIED.);
#807=B_SPLINE_CURVE_WITH_KNOTS('',3,(#70947,#70948,#70949,#70950,#70951,
#70952,#70953,#70954,#70955,#70956,#70957,#70958,#70959,#70960,#70961,#70962,
#70963,#70964,#70965,#70966,#70967,#70968,#70969,#70970,#70971,#70972,#70973,
#70974,#70975,#70976,#70977,#70978,#70979,#70980,#70981,#70982,#70983,#70984,
#70985,#70986,#70987,#70988,#70989),.UNSPECIFIED.,.F.,.F.,(4,3,3,3,3,3,
3,3,3,3,3,3,3,3,4),(-0.459480514361606,-0.416804016852846,-0.373075117462449,
-0.369143093793734,-0.322563532475183,-0.299796705045319,-0.27858084573658,
-0.220296138014231,-0.206166571473084,-0.154844056501134,-0.125504378000612,
-0.0790936974906717,-0.0343817313041713,-0.0161363994082055,0.),
 .UNSPECIFIED.);
#808=B_SPLINE_CURVE_WITH_KNOTS('',3,(#70993,#70994,#70995,#70996,#70997,
#70998,#70999,#71000,#71001,#71002,#71003,#71004,#71005,#71006,#71007,#71008,
#71009,#71010,#71011,#71012,#71013,#71014,#71015,#71016,#71017,#71018,#71019,
#71020,#71021,#71022,#71023,#71024,#71025,#71026,#71027,#71028,#71029),
 .UNSPECIFIED.,.F.,.F.,(4,3,3,3,3,3,3,3,3,3,3,3,4),(-0.459480514362015,
-0.443345601466716,-0.398421538221141,-0.369143093793975,-0.320538018706025,
-0.278580845736683,-0.221183542332208,-0.206166571473132,-0.159724811114509,
-0.125504378000635,-0.0807834581110674,-0.0377756277020226,0.),
 .UNSPECIFIED.);
#809=B_SPLINE_CURVE_WITH_KNOTS('',3,(#71033,#71034,#71035,#71036,#71037,
#71038,#71039,#71040,#71041,#71042,#71043,#71044,#71045,#71046,#71047,#71048,
#71049,#71050,#71051,#71052,#71053,#71054,#71055,#71056,#71057,#71058,#71059,
#71060,#71061,#71062,#71063,#71064,#71065,#71066,#71067,#71068,#71069),
 .UNSPECIFIED.,.F.,.F.,(4,3,3,3,3,3,3,3,3,3,3,3,4),(-0.459480514361764,
-0.443345601466454,-0.398418086430042,-0.369143093793749,-0.320534667578597,
-0.278580845736547,-0.221174845680044,-0.206166571473085,-0.159724811114519,
-0.12550437800065,-0.0807878344311111,-0.0377841697597962,0.),
 .UNSPECIFIED.);
#810=B_SPLINE_CURVE_WITH_KNOTS('',3,(#71073,#71074,#71075,#71076,#71077,
#71078,#71079,#71080,#71081,#71082,#71083,#71084,#71085,#71086,#71087,#71088,
#71089,#71090,#71091,#71092,#71093,#71094,#71095,#71096,#71097,#71098,#71099,
#71100,#71101,#71102,#71103,#71104,#71105,#71106,#71107,#71108,#71109,#71110,
#71111,#71112,#71113,#71114,#71115),.UNSPECIFIED.,.F.,.F.,(4,3,3,3,3,3,
3,3,3,3,3,3,3,3,4),(-0.45948051436171,-0.416804016851814,-0.373075117460496,
-0.369143093793726,-0.322563532475871,-0.299796705045298,-0.278580845736541,
-0.22029613801833,-0.206166571473066,-0.154844056502094,-0.125504378000622,
-0.0790936974907238,-0.0343817313044943,-0.0161363994082399,0.),
 .UNSPECIFIED.);
#811=B_SPLINE_CURVE_WITH_KNOTS('',3,(#71118,#71119,#71120,#71121,#71122,
#71123,#71124,#71125,#71126,#71127,#71128,#71129,#71130,#71131,#71132,#71133,
#71134,#71135,#71136),.UNSPECIFIED.,.F.,.F.,(4,3,3,3,3,3,4),(-0.459480514361756,
-0.443345601466462,-0.398421538221248,-0.369143093793824,-0.320538018705387,
-0.278580845736626,-0.229761503419508),.UNSPECIFIED.);
#812=B_SPLINE_CURVE_WITH_KNOTS('',3,(#71162,#71163,#71164,#71165),
 .UNSPECIFIED.,.F.,.F.,(4,4),(0.906486097601391,1.2005720772214),
 .UNSPECIFIED.);
#813=B_SPLINE_CURVE_WITH_KNOTS('',3,(#71167,#71168,#71169,#71170,#71171,
#71172),.UNSPECIFIED.,.F.,.F.,(4,2,4),(-0.0856551294938672,-0.0428224901510306,
0.),.UNSPECIFIED.);
#814=B_SPLINE_CURVE_WITH_KNOTS('',3,(#71174,#71175,#71176,#71177,#71178,
#71179),.UNSPECIFIED.,.F.,.F.,(4,1,1,4),(-1.19740918080757,-0.889549641576921,
-0.578527205932438,-0.115156448879797),.UNSPECIFIED.);
#815=B_SPLINE_CURVE_WITH_KNOTS('',3,(#71181,#71182,#71183,#71184,#71185,
#71186),.UNSPECIFIED.,.F.,.F.,(4,2,4),(-0.0856551215567144,-0.0428321834459229,
0.),.UNSPECIFIED.);
#816=B_SPLINE_CURVE_WITH_KNOTS('',3,(#71187,#71188,#71189,#71190),
 .UNSPECIFIED.,.F.,.F.,(4,4),(0.111993552465714,0.406079532085727),
 .UNSPECIFIED.);
#817=B_SPLINE_CURVE_WITH_KNOTS('',3,(#71216,#71217,#71218,#71219),
 .UNSPECIFIED.,.F.,.F.,(4,4),(0.90648609760139,1.2005720772214),
 .UNSPECIFIED.);
#818=B_SPLINE_CURVE_WITH_KNOTS('',3,(#71221,#71222,#71223,#71224,#71225,
#71226),.UNSPECIFIED.,.F.,.F.,(4,2,4),(-0.0856551294979727,-0.0428224901518006,
0.),.UNSPECIFIED.);
#819=B_SPLINE_CURVE_WITH_KNOTS('',3,(#71228,#71229,#71230,#71231,#71232,
#71233),.UNSPECIFIED.,.F.,.F.,(4,1,1,4),(-1.19740918080757,-0.889549641576921,
-0.578527205932438,-0.115156448879797),.UNSPECIFIED.);
#820=B_SPLINE_CURVE_WITH_KNOTS('',3,(#71234,#71235,#71236,#71237,#71238,
#71239),.UNSPECIFIED.,.F.,.F.,(4,2,4),(-0.0856551215544335,-0.0428321834456351,
0.),.UNSPECIFIED.);
#821=B_SPLINE_CURVE_WITH_KNOTS('',3,(#71240,#71241,#71242,#71243),
 .UNSPECIFIED.,.F.,.F.,(4,4),(0.111993552465714,0.406079532085726),
 .UNSPECIFIED.);
#822=B_SPLINE_CURVE_WITH_KNOTS('',3,(#71246,#71247,#71248,#71249),
 .UNSPECIFIED.,.F.,.F.,(4,4),(0.111993552465713,0.406079532085725),
 .UNSPECIFIED.);
#823=B_SPLINE_CURVE_WITH_KNOTS('',3,(#71252,#71253,#71254,#71255),
 .UNSPECIFIED.,.F.,.F.,(4,4),(0.111993552465714,0.406079532085727),
 .UNSPECIFIED.);
#824=B_SPLINE_CURVE_WITH_KNOTS('',3,(#71256,#71257,#71258,#71259),
 .UNSPECIFIED.,.F.,.F.,(4,4),(0.906486097601392,1.2005720772214),
 .UNSPECIFIED.);
#825=B_SPLINE_CURVE_WITH_KNOTS('',3,(#71262,#71263,#71264,#71265),
 .UNSPECIFIED.,.F.,.F.,(4,4),(0.111993552465714,0.406079532085725),
 .UNSPECIFIED.);
#826=B_SPLINE_CURVE_WITH_KNOTS('',3,(#71266,#71267,#71268,#71269),
 .UNSPECIFIED.,.F.,.F.,(4,4),(0.906486097601392,1.2005720772214),
 .UNSPECIFIED.);
#827=B_SPLINE_CURVE_WITH_KNOTS('',3,(#71272,#71273,#71274,#71275),
 .UNSPECIFIED.,.F.,.F.,(4,4),(0.111993552465714,0.406079532085727),
 .UNSPECIFIED.);
#828=B_SPLINE_CURVE_WITH_KNOTS('',3,(#71276,#71277,#71278,#71279),
 .UNSPECIFIED.,.F.,.F.,(4,4),(0.906486097601392,1.20057207722141),
 .UNSPECIFIED.);
#829=B_SPLINE_CURVE_WITH_KNOTS('',3,(#71281,#71282,#71283,#71284),
 .UNSPECIFIED.,.F.,.F.,(4,4),(0.906486097601391,1.2005720772214),
 .UNSPECIFIED.);
#830=B_SPLINE_CURVE_WITH_KNOTS('',3,(#71310,#71311,#71312,#71313,#71314,
#71315),.UNSPECIFIED.,.F.,.F.,(4,2,4),(-0.0856551294832383,-0.0428224901484855,
0.),.UNSPECIFIED.);
#831=B_SPLINE_CURVE_WITH_KNOTS('',3,(#71317,#71318,#71319,#71320,#71321,
#71322),.UNSPECIFIED.,.F.,.F.,(4,1,1,4),(-1.19740918080757,-0.734038423754679,
-0.423015988110196,-0.115156448879796),.UNSPECIFIED.);
#832=B_SPLINE_CURVE_WITH_KNOTS('',3,(#71323,#71324,#71325,#71326,#71327,
#71328),.UNSPECIFIED.,.F.,.F.,(4,2,4),(-0.0856551215544496,-0.0428321834445534,
0.),.UNSPECIFIED.);
#833=B_SPLINE_CURVE_WITH_KNOTS('',3,(#71367,#71368,#71369,#71370,#71371,
#71372),.UNSPECIFIED.,.F.,.F.,(4,2,4),(-0.0856551215520138,-0.042832183445196,
0.),.UNSPECIFIED.);
#834=B_SPLINE_CURVE_WITH_KNOTS('',3,(#71398,#71399,#71400,#71401,#71402,
#71403),.UNSPECIFIED.,.F.,.F.,(4,2,4),(-0.0856551294860877,-0.0428224901488512,
0.),.UNSPECIFIED.);
#835=B_SPLINE_CURVE_WITH_KNOTS('',3,(#71405,#71406,#71407,#71408,#71409,
#71410),.UNSPECIFIED.,.F.,.F.,(4,2,4),(-0.0856551215570029,-0.0428321834468217,
0.),.UNSPECIFIED.);
#836=B_SPLINE_CURVE_WITH_KNOTS('',3,(#71415,#71416,#71417,#71418,#71419,
#71420),.UNSPECIFIED.,.F.,.F.,(4,2,4),(-0.0856551294977852,-0.0428224901521715,
0.),.UNSPECIFIED.);
#837=B_SPLINE_CURVE_WITH_KNOTS('',3,(#71423,#71424,#71425,#71426,#71427,
#71428),.UNSPECIFIED.,.F.,.F.,(4,2,4),(-0.085655129500155,-0.0428224901528902,
0.),.UNSPECIFIED.);
#838=B_SPLINE_CURVE_WITH_KNOTS('',3,(#71430,#71431,#71432,#71433,#71434,
#71435),.UNSPECIFIED.,.F.,.F.,(4,2,4),(-0.0856551215531883,-0.0428321834438049,
0.),.UNSPECIFIED.);
#839=B_SPLINE_CURVE_WITH_KNOTS('',3,(#71461,#71462,#71463,#71464,#71465,
#71466),.UNSPECIFIED.,.F.,.F.,(4,1,1,4),(-1.19740918080757,-0.73403842375468,
-0.423015988110197,-0.115156448879797),.UNSPECIFIED.);
#840=B_SPLINE_CURVE_WITH_KNOTS('',3,(#71494,#71495,#71496,#71497,#71498,
#71499),.UNSPECIFIED.,.F.,.F.,(4,1,1,4),(-1.19740918080757,-0.889549641576922,
-0.578527205932439,-0.115156448879796),.UNSPECIFIED.);
#841=B_SPLINE_CURVE_WITH_KNOTS('',3,(#71530,#71531,#71532,#71533,#71534,
#71535),.UNSPECIFIED.,.F.,.F.,(4,1,1,4),(-1.19740918080757,-0.889549641576921,
-0.578527205932438,-0.115156448879797),.UNSPECIFIED.);
#1332=FACE_BOUND('',#7493,.T.);
#1333=FACE_BOUND('',#7523,.T.);
#1334=FACE_BOUND('',#7532,.T.);
#2959=PLANE('',#37598);
#2960=PLANE('',#37600);
#2961=PLANE('',#37601);
#2962=PLANE('',#37602);
#2963=PLANE('',#37603);
#2964=PLANE('',#37604);
#2965=PLANE('',#37605);
#2966=PLANE('',#37606);
#2967=PLANE('',#37607);
#2968=PLANE('',#37608);
#2969=PLANE('',#37609);
#2970=PLANE('',#37610);
#2971=PLANE('',#37611);
#2972=PLANE('',#37612);
#2973=PLANE('',#37613);
#2974=PLANE('',#37614);
#2975=PLANE('',#37615);
#2976=PLANE('',#37616);
#2977=PLANE('',#37617);
#2978=PLANE('',#37618);
#2979=PLANE('',#37619);
#2980=PLANE('',#37620);
#2981=PLANE('',#37621);
#2982=PLANE('',#37622);
#2983=PLANE('',#37623);
#2984=PLANE('',#37624);
#2985=PLANE('',#37625);
#2986=PLANE('',#37627);
#2987=PLANE('',#37628);
#2988=PLANE('',#37629);
#2989=PLANE('',#37630);
#2990=PLANE('',#37631);
#2991=PLANE('',#37637);
#3138=CYLINDRICAL_SURFACE('',#37639,6.4);
#5185=FACE_OUTER_BOUND('',#7482,.T.);
#5186=FACE_OUTER_BOUND('',#7483,.T.);
#5187=FACE_OUTER_BOUND('',#7484,.T.);
#5188=FACE_OUTER_BOUND('',#7485,.T.);
#5189=FACE_OUTER_BOUND('',#7486,.T.);
#5190=FACE_OUTER_BOUND('',#7487,.T.);
#5191=FACE_OUTER_BOUND('',#7488,.T.);
#5192=FACE_OUTER_BOUND('',#7489,.T.);
#5193=FACE_OUTER_BOUND('',#7490,.T.);
#5194=FACE_OUTER_BOUND('',#7491,.T.);
#5195=FACE_OUTER_BOUND('',#7492,.T.);
#5196=FACE_OUTER_BOUND('',#7494,.T.);
#5197=FACE_OUTER_BOUND('',#7495,.T.);
#5198=FACE_OUTER_BOUND('',#7496,.T.);
#5199=FACE_OUTER_BOUND('',#7497,.T.);
#5200=FACE_OUTER_BOUND('',#7498,.T.);
#5201=FACE_OUTER_BOUND('',#7499,.T.);
#5202=FACE_OUTER_BOUND('',#7500,.T.);
#5203=FACE_OUTER_BOUND('',#7501,.T.);
#5204=FACE_OUTER_BOUND('',#7502,.T.);
#5205=FACE_OUTER_BOUND('',#7503,.T.);
#5206=FACE_OUTER_BOUND('',#7504,.T.);
#5207=FACE_OUTER_BOUND('',#7505,.T.);
#5208=FACE_OUTER_BOUND('',#7506,.T.);
#5209=FACE_OUTER_BOUND('',#7507,.T.);
#5210=FACE_OUTER_BOUND('',#7508,.T.);
#5211=FACE_OUTER_BOUND('',#7509,.T.);
#5212=FACE_OUTER_BOUND('',#7510,.T.);
#5213=FACE_OUTER_BOUND('',#7511,.T.);
#5214=FACE_OUTER_BOUND('',#7512,.T.);
#5215=FACE_OUTER_BOUND('',#7513,.T.);
#5216=FACE_OUTER_BOUND('',#7514,.T.);
#5217=FACE_OUTER_BOUND('',#7515,.T.);
#5218=FACE_OUTER_BOUND('',#7516,.T.);
#5219=FACE_OUTER_BOUND('',#7517,.T.);
#5220=FACE_OUTER_BOUND('',#7518,.T.);
#5221=FACE_OUTER_BOUND('',#7519,.T.);
#5222=FACE_OUTER_BOUND('',#7520,.T.);
#5223=FACE_OUTER_BOUND('',#7521,.T.);
#5224=FACE_OUTER_BOUND('',#7522,.T.);
#5225=FACE_OUTER_BOUND('',#7524,.T.);
#5226=FACE_OUTER_BOUND('',#7525,.T.);
#5227=FACE_OUTER_BOUND('',#7526,.T.);
#5228=FACE_OUTER_BOUND('',#7527,.T.);
#5229=FACE_OUTER_BOUND('',#7528,.T.);
#5230=FACE_OUTER_BOUND('',#7529,.T.);
#5231=FACE_OUTER_BOUND('',#7530,.T.);
#5232=FACE_OUTER_BOUND('',#7531,.T.);
#5233=FACE_OUTER_BOUND('',#7533,.T.);
#7482=EDGE_LOOP('',(#31724,#31725,#31726,#31727,#31728,#31729,#31730,#31731,
#31732,#31733,#31734,#31735,#31736,#31737,#31738,#31739));
#7483=EDGE_LOOP('',(#31740,#31741,#31742,#31743,#31744,#31745));
#7484=EDGE_LOOP('',(#31746,#31747,#31748,#31749,#31750,#31751,#31752));
#7485=EDGE_LOOP('',(#31753,#31754,#31755));
#7486=EDGE_LOOP('',(#31756,#31757,#31758));
#7487=EDGE_LOOP('',(#31759,#31760,#31761));
#7488=EDGE_LOOP('',(#31762,#31763,#31764));
#7489=EDGE_LOOP('',(#31765,#31766,#31767));
#7490=EDGE_LOOP('',(#31768,#31769,#31770));
#7491=EDGE_LOOP('',(#31771,#31772,#31773,#31774,#31775,#31776));
#7492=EDGE_LOOP('',(#31777));
#7493=EDGE_LOOP('',(#31778));
#7494=EDGE_LOOP('',(#31779,#31780,#31781));
#7495=EDGE_LOOP('',(#31782,#31783,#31784));
#7496=EDGE_LOOP('',(#31785,#31786,#31787));
#7497=EDGE_LOOP('',(#31788,#31789,#31790,#31791));
#7498=EDGE_LOOP('',(#31792,#31793,#31794));
#7499=EDGE_LOOP('',(#31795,#31796,#31797));
#7500=EDGE_LOOP('',(#31798,#31799,#31800));
#7501=EDGE_LOOP('',(#31801,#31802,#31803));
#7502=EDGE_LOOP('',(#31804,#31805,#31806,#31807));
#7503=EDGE_LOOP('',(#31808,#31809,#31810));
#7504=EDGE_LOOP('',(#31811,#31812,#31813));
#7505=EDGE_LOOP('',(#31814,#31815,#31816,#31817));
#7506=EDGE_LOOP('',(#31818,#31819,#31820));
#7507=EDGE_LOOP('',(#31821,#31822,#31823));
#7508=EDGE_LOOP('',(#31824,#31825,#31826));
#7509=EDGE_LOOP('',(#31827,#31828,#31829,#31830,#31831,#31832));
#7510=EDGE_LOOP('',(#31833,#31834,#31835,#31836));
#7511=EDGE_LOOP('',(#31837,#31838,#31839,#31840,#31841,#31842));
#7512=EDGE_LOOP('',(#31843,#31844,#31845,#31846));
#7513=EDGE_LOOP('',(#31847,#31848,#31849,#31850));
#7514=EDGE_LOOP('',(#31851,#31852,#31853,#31854,#31855,#31856));
#7515=EDGE_LOOP('',(#31857,#31858,#31859,#31860));
#7516=EDGE_LOOP('',(#31861,#31862,#31863,#31864));
#7517=EDGE_LOOP('',(#31865,#31866,#31867,#31868));
#7518=EDGE_LOOP('',(#31869,#31870,#31871,#31872));
#7519=EDGE_LOOP('',(#31873,#31874,#31875,#31876));
#7520=EDGE_LOOP('',(#31877,#31878,#31879,#31880));
#7521=EDGE_LOOP('',(#31881,#31882,#31883,#31884));
#7522=EDGE_LOOP('',(#31885,#31886,#31887,#31888,#31889,#31890));
#7523=EDGE_LOOP('',(#31891));
#7524=EDGE_LOOP('',(#31892,#31893,#31894,#31895));
#7525=EDGE_LOOP('',(#31896,#31897,#31898,#31899));
#7526=EDGE_LOOP('',(#31900,#31901,#31902,#31903));
#7527=EDGE_LOOP('',(#31904,#31905,#31906,#31907));
#7528=EDGE_LOOP('',(#31908,#31909,#31910,#31911));
#7529=EDGE_LOOP('',(#31912,#31913,#31914,#31915,#31916));
#7530=EDGE_LOOP('',(#31917,#31918,#31919,#31920));
#7531=EDGE_LOOP('',(#31921));
#7532=EDGE_LOOP('',(#31922));
#7533=EDGE_LOOP('',(#31923,#31924,#31925,#31926,#31927));
#10532=LINE('',#70883,#13582);
#10533=LINE('',#71335,#13583);
#10534=LINE('',#71337,#13584);
#10535=LINE('',#71338,#13585);
#10536=LINE('',#71342,#13586);
#10537=LINE('',#71344,#13587);
#10538=LINE('',#71345,#13588);
#10539=LINE('',#71349,#13589);
#10540=LINE('',#71351,#13590);
#10541=LINE('',#71352,#13591);
#10542=LINE('',#71354,#13592);
#10543=LINE('',#71355,#13593);
#10544=LINE('',#71357,#13594);
#10545=LINE('',#71361,#13595);
#10546=LINE('',#71363,#13596);
#10547=LINE('',#71364,#13597);
#10548=LINE('',#71373,#13598);
#10549=LINE('',#71377,#13599);
#10550=LINE('',#71379,#13600);
#10551=LINE('',#71380,#13601);
#10552=LINE('',#71382,#13602);
#10553=LINE('',#71383,#13603);
#10554=LINE('',#71385,#13604);
#10555=LINE('',#71389,#13605);
#10556=LINE('',#71391,#13606);
#10557=LINE('',#71392,#13607);
#10558=LINE('',#71394,#13608);
#10559=LINE('',#71395,#13609);
#10560=LINE('',#71411,#13610);
#10561=LINE('',#71414,#13611);
#10562=LINE('',#71436,#13612);
#10563=LINE('',#71468,#13613);
#10564=LINE('',#71469,#13614);
#10565=LINE('',#71501,#13615);
#10566=LINE('',#71502,#13616);
#10567=LINE('',#71504,#13617);
#10568=LINE('',#71505,#13618);
#10569=LINE('',#71537,#13619);
#10570=LINE('',#71538,#13620);
#10571=LINE('',#71540,#13621);
#10572=LINE('',#71541,#13622);
#10573=LINE('',#71543,#13623);
#10574=LINE('',#71544,#13624);
#10575=LINE('',#71546,#13625);
#10576=LINE('',#71547,#13626);
#10577=LINE('',#71549,#13627);
#10578=LINE('',#71550,#13628);
#10579=LINE('',#71552,#13629);
#10580=LINE('',#71553,#13630);
#10581=LINE('',#71567,#13631);
#10582=LINE('',#71571,#13632);
#10583=LINE('',#71577,#13633);
#13582=VECTOR('',#47101,8.9203817394342);
#13583=VECTOR('',#47132,10.);
#13584=VECTOR('',#47133,10.);
#13585=VECTOR('',#47134,10.);
#13586=VECTOR('',#47137,10.);
#13587=VECTOR('',#47138,10.);
#13588=VECTOR('',#47139,10.);
#13589=VECTOR('',#47142,10.);
#13590=VECTOR('',#47143,10.);
#13591=VECTOR('',#47144,10.);
#13592=VECTOR('',#47147,10.);
#13593=VECTOR('',#47148,10.);
#13594=VECTOR('',#47151,10.);
#13595=VECTOR('',#47154,10.);
#13596=VECTOR('',#47155,10.);
#13597=VECTOR('',#47156,10.);
#13598=VECTOR('',#47159,10.);
#13599=VECTOR('',#47162,10.);
#13600=VECTOR('',#47163,10.);
#13601=VECTOR('',#47164,10.);
#13602=VECTOR('',#47167,10.);
#13603=VECTOR('',#47168,10.);
#13604=VECTOR('',#47171,10.);
#13605=VECTOR('',#47174,10.);
#13606=VECTOR('',#47175,10.);
#13607=VECTOR('',#47176,10.);
#13608=VECTOR('',#47179,10.);
#13609=VECTOR('',#47180,10.);
#13610=VECTOR('',#47183,10.);
#13611=VECTOR('',#47186,10.);
#13612=VECTOR('',#47189,10.);
#13613=VECTOR('',#47192,10.);
#13614=VECTOR('',#47193,10.);
#13615=VECTOR('',#47196,10.);
#13616=VECTOR('',#47197,10.);
#13617=VECTOR('',#47200,10.);
#13618=VECTOR('',#47201,10.);
#13619=VECTOR('',#47204,10.);
#13620=VECTOR('',#47205,10.);
#13621=VECTOR('',#47208,10.);
#13622=VECTOR('',#47209,10.);
#13623=VECTOR('',#47212,10.);
#13624=VECTOR('',#47213,10.);
#13625=VECTOR('',#47216,10.);
#13626=VECTOR('',#47217,10.);
#13627=VECTOR('',#47220,10.);
#13628=VECTOR('',#47221,10.);
#13629=VECTOR('',#47224,10.);
#13630=VECTOR('',#47225,10.);
#13631=VECTOR('',#47246,6.8);
#13632=VECTOR('',#47251,8.35);
#13633=VECTOR('',#47260,6.4);
#14519=CIRCLE('',#37585,8.45882352941176);
#14520=CIRCLE('',#37586,9.38193994945664);
#14521=CIRCLE('',#37587,9.38193994945664);
#14522=CIRCLE('',#37588,9.38193994945664);
#14523=CIRCLE('',#37589,9.38193994945664);
#14524=CIRCLE('',#37590,9.38193994945664);
#14525=CIRCLE('',#37591,9.38193994945664);
#14526=CIRCLE('',#37599,7.1);
#14527=CIRCLE('',#37626,8.925);
#14528=CIRCLE('',#37633,6.4);
#14529=CIRCLE('',#37634,6.4);
#14530=CIRCLE('',#37636,7.2);
#14531=CIRCLE('',#37638,6.4);
#17397=VERTEX_POINT('',#70880);
#17398=VERTEX_POINT('',#70882);
#17399=VERTEX_POINT('',#70884);
#17400=VERTEX_POINT('',#70904);
#17401=VERTEX_POINT('',#70906);
#17402=VERTEX_POINT('',#70944);
#17403=VERTEX_POINT('',#70946);
#17404=VERTEX_POINT('',#70990);
#17405=VERTEX_POINT('',#70992);
#17406=VERTEX_POINT('',#71030);
#17407=VERTEX_POINT('',#71032);
#17408=VERTEX_POINT('',#71070);
#17409=VERTEX_POINT('',#71072);
#17410=VERTEX_POINT('',#71116);
#17411=VERTEX_POINT('',#71161);
#17412=VERTEX_POINT('',#71166);
#17413=VERTEX_POINT('',#71173);
#17414=VERTEX_POINT('',#71180);
#17415=VERTEX_POINT('',#71215);
#17416=VERTEX_POINT('',#71220);
#17417=VERTEX_POINT('',#71227);
#17418=VERTEX_POINT('',#71251);
#17419=VERTEX_POINT('',#71261);
#17420=VERTEX_POINT('',#71271);
#17421=VERTEX_POINT('',#71309);
#17422=VERTEX_POINT('',#71316);
#17423=VERTEX_POINT('',#71330);
#17424=VERTEX_POINT('',#71333);
#17425=VERTEX_POINT('',#71334);
#17426=VERTEX_POINT('',#71336);
#17427=VERTEX_POINT('',#71340);
#17428=VERTEX_POINT('',#71341);
#17429=VERTEX_POINT('',#71343);
#17430=VERTEX_POINT('',#71347);
#17431=VERTEX_POINT('',#71348);
#17432=VERTEX_POINT('',#71350);
#17433=VERTEX_POINT('',#71359);
#17434=VERTEX_POINT('',#71360);
#17435=VERTEX_POINT('',#71362);
#17436=VERTEX_POINT('',#71366);
#17437=VERTEX_POINT('',#71375);
#17438=VERTEX_POINT('',#71376);
#17439=VERTEX_POINT('',#71378);
#17440=VERTEX_POINT('',#71387);
#17441=VERTEX_POINT('',#71388);
#17442=VERTEX_POINT('',#71390);
#17443=VERTEX_POINT('',#71397);
#17444=VERTEX_POINT('',#71404);
#17445=VERTEX_POINT('',#71413);
#17446=VERTEX_POINT('',#71422);
#17447=VERTEX_POINT('',#71429);
#17448=VERTEX_POINT('',#71556);
#17449=VERTEX_POINT('',#71564);
#17450=VERTEX_POINT('',#71565);
#17451=VERTEX_POINT('',#71570);
#17452=VERTEX_POINT('',#71574);
#22176=EDGE_CURVE('',#17397,#17397,#14519,.T.);
#22177=EDGE_CURVE('',#17397,#17398,#10532,.T.);
#22178=EDGE_CURVE('',#17398,#17399,#805,.T.);
#22179=EDGE_CURVE('',#17399,#17400,#14520,.T.);
#22180=EDGE_CURVE('',#17400,#17401,#806,.T.);
#22181=EDGE_CURVE('',#17401,#17402,#14521,.T.);
#22182=EDGE_CURVE('',#17402,#17403,#807,.T.);
#22183=EDGE_CURVE('',#17403,#17404,#14522,.T.);
#22184=EDGE_CURVE('',#17404,#17405,#808,.T.);
#22185=EDGE_CURVE('',#17405,#17406,#14523,.T.);
#22186=EDGE_CURVE('',#17406,#17407,#809,.T.);
#22187=EDGE_CURVE('',#17407,#17408,#14524,.T.);
#22188=EDGE_CURVE('',#17408,#17409,#810,.T.);
#22189=EDGE_CURVE('',#17409,#17410,#14525,.T.);
#22190=EDGE_CURVE('',#17410,#17398,#811,.T.);
#22191=EDGE_CURVE('',#17400,#17411,#812,.T.);
#22192=EDGE_CURVE('',#17411,#17412,#813,.F.);
#22193=EDGE_CURVE('',#17412,#17413,#814,.T.);
#22194=EDGE_CURVE('',#17413,#17414,#815,.F.);
#22195=EDGE_CURVE('',#17414,#17401,#816,.T.);
#22196=EDGE_CURVE('',#17410,#17415,#817,.T.);
#22197=EDGE_CURVE('',#17415,#17416,#818,.F.);
#22198=EDGE_CURVE('',#17416,#17417,#819,.T.);
#22199=EDGE_CURVE('',#17417,#17411,#820,.F.);
#22200=EDGE_CURVE('',#17411,#17399,#821,.T.);
#22201=EDGE_CURVE('',#17415,#17409,#822,.T.);
#22202=EDGE_CURVE('',#17418,#17407,#823,.T.);
#22203=EDGE_CURVE('',#17408,#17418,#824,.T.);
#22204=EDGE_CURVE('',#17419,#17405,#825,.T.);
#22205=EDGE_CURVE('',#17406,#17419,#826,.T.);
#22206=EDGE_CURVE('',#17420,#17403,#827,.T.);
#22207=EDGE_CURVE('',#17404,#17420,#828,.T.);
#22208=EDGE_CURVE('',#17402,#17414,#829,.T.);
#22209=EDGE_CURVE('',#17418,#17421,#830,.F.);
#22210=EDGE_CURVE('',#17421,#17422,#831,.T.);
#22211=EDGE_CURVE('',#17422,#17415,#832,.F.);
#22212=EDGE_CURVE('',#17423,#17423,#14526,.T.);
#22213=EDGE_CURVE('',#17424,#17425,#10533,.T.);
#22214=EDGE_CURVE('',#17426,#17424,#10534,.T.);
#22215=EDGE_CURVE('',#17425,#17426,#10535,.T.);
#22216=EDGE_CURVE('',#17427,#17428,#10536,.T.);
#22217=EDGE_CURVE('',#17429,#17427,#10537,.T.);
#22218=EDGE_CURVE('',#17428,#17429,#10538,.T.);
#22219=EDGE_CURVE('',#17430,#17431,#10539,.T.);
#22220=EDGE_CURVE('',#17432,#17430,#10540,.T.);
#22221=EDGE_CURVE('',#17431,#17432,#10541,.T.);
#22222=EDGE_CURVE('',#17430,#17425,#10542,.T.);
#22223=EDGE_CURVE('',#17426,#17432,#10543,.T.);
#22224=EDGE_CURVE('',#17416,#17422,#10544,.T.);
#22225=EDGE_CURVE('',#17433,#17434,#10545,.T.);
#22226=EDGE_CURVE('',#17435,#17433,#10546,.T.);
#22227=EDGE_CURVE('',#17434,#17435,#10547,.T.);
#22228=EDGE_CURVE('',#17436,#17418,#833,.F.);
#22229=EDGE_CURVE('',#17421,#17436,#10548,.T.);
#22230=EDGE_CURVE('',#17437,#17438,#10549,.T.);
#22231=EDGE_CURVE('',#17439,#17437,#10550,.T.);
#22232=EDGE_CURVE('',#17438,#17439,#10551,.T.);
#22233=EDGE_CURVE('',#17437,#17431,#10552,.T.);
#22234=EDGE_CURVE('',#17432,#17439,#10553,.T.);
#22235=EDGE_CURVE('',#17412,#17417,#10554,.T.);
#22236=EDGE_CURVE('',#17440,#17441,#10555,.T.);
#22237=EDGE_CURVE('',#17442,#17440,#10556,.T.);
#22238=EDGE_CURVE('',#17441,#17442,#10557,.T.);
#22239=EDGE_CURVE('',#17433,#17442,#10558,.T.);
#22240=EDGE_CURVE('',#17440,#17435,#10559,.T.);
#22241=EDGE_CURVE('',#17419,#17443,#834,.F.);
#22242=EDGE_CURVE('',#17444,#17419,#835,.F.);
#22243=EDGE_CURVE('',#17443,#17444,#10560,.T.);
#22244=EDGE_CURVE('',#17445,#17413,#10561,.T.);
#22245=EDGE_CURVE('',#17414,#17445,#836,.F.);
#22246=EDGE_CURVE('',#17420,#17446,#837,.F.);
#22247=EDGE_CURVE('',#17447,#17420,#838,.F.);
#22248=EDGE_CURVE('',#17446,#17447,#10562,.T.);
#22249=EDGE_CURVE('',#17445,#17447,#839,.T.);
#22250=EDGE_CURVE('',#17447,#17441,#10563,.T.);
#22251=EDGE_CURVE('',#17442,#17446,#10564,.T.);
#22252=EDGE_CURVE('',#17446,#17444,#840,.T.);
#22253=EDGE_CURVE('',#17413,#17437,#10565,.T.);
#22254=EDGE_CURVE('',#17438,#17445,#10566,.T.);
#22255=EDGE_CURVE('',#17444,#17433,#10567,.T.);
#22256=EDGE_CURVE('',#17434,#17443,#10568,.T.);
#22257=EDGE_CURVE('',#17443,#17436,#841,.T.);
#22258=EDGE_CURVE('',#17441,#17438,#10569,.T.);
#22259=EDGE_CURVE('',#17439,#17440,#10570,.T.);
#22260=EDGE_CURVE('',#17417,#17430,#10571,.T.);
#22261=EDGE_CURVE('',#17431,#17412,#10572,.T.);
#22262=EDGE_CURVE('',#17436,#17427,#10573,.T.);
#22263=EDGE_CURVE('',#17428,#17421,#10574,.T.);
#22264=EDGE_CURVE('',#17427,#17434,#10575,.T.);
#22265=EDGE_CURVE('',#17435,#17429,#10576,.T.);
#22266=EDGE_CURVE('',#17422,#17424,#10577,.T.);
#22267=EDGE_CURVE('',#17425,#17416,#10578,.T.);
#22268=EDGE_CURVE('',#17424,#17428,#10579,.T.);
#22269=EDGE_CURVE('',#17429,#17426,#10580,.T.);
#22270=EDGE_CURVE('',#17448,#17448,#14527,.T.);
#22271=EDGE_CURVE('',#17449,#17450,#14528,.T.);
#22272=EDGE_CURVE('',#17449,#17423,#10581,.T.);
#22273=EDGE_CURVE('',#17450,#17449,#14529,.T.);
#22274=EDGE_CURVE('',#17448,#17451,#10582,.T.);
#22275=EDGE_CURVE('',#17451,#17451,#14530,.T.);
#22276=EDGE_CURVE('',#17452,#17452,#14531,.T.);
#22277=EDGE_CURVE('',#17450,#17452,#10583,.T.);
#31724=ORIENTED_EDGE('',*,*,#22176,.T.);
#31725=ORIENTED_EDGE('',*,*,#22177,.T.);
#31726=ORIENTED_EDGE('',*,*,#22178,.T.);
#31727=ORIENTED_EDGE('',*,*,#22179,.T.);
#31728=ORIENTED_EDGE('',*,*,#22180,.T.);
#31729=ORIENTED_EDGE('',*,*,#22181,.T.);
#31730=ORIENTED_EDGE('',*,*,#22182,.T.);
#31731=ORIENTED_EDGE('',*,*,#22183,.T.);
#31732=ORIENTED_EDGE('',*,*,#22184,.T.);
#31733=ORIENTED_EDGE('',*,*,#22185,.T.);
#31734=ORIENTED_EDGE('',*,*,#22186,.T.);
#31735=ORIENTED_EDGE('',*,*,#22187,.T.);
#31736=ORIENTED_EDGE('',*,*,#22188,.T.);
#31737=ORIENTED_EDGE('',*,*,#22189,.T.);
#31738=ORIENTED_EDGE('',*,*,#22190,.T.);
#31739=ORIENTED_EDGE('',*,*,#22177,.F.);
#31740=ORIENTED_EDGE('',*,*,#22180,.F.);
#31741=ORIENTED_EDGE('',*,*,#22191,.T.);
#31742=ORIENTED_EDGE('',*,*,#22192,.T.);
#31743=ORIENTED_EDGE('',*,*,#22193,.T.);
#31744=ORIENTED_EDGE('',*,*,#22194,.T.);
#31745=ORIENTED_EDGE('',*,*,#22195,.T.);
#31746=ORIENTED_EDGE('',*,*,#22190,.F.);
#31747=ORIENTED_EDGE('',*,*,#22196,.T.);
#31748=ORIENTED_EDGE('',*,*,#22197,.T.);
#31749=ORIENTED_EDGE('',*,*,#22198,.T.);
#31750=ORIENTED_EDGE('',*,*,#22199,.T.);
#31751=ORIENTED_EDGE('',*,*,#22200,.T.);
#31752=ORIENTED_EDGE('',*,*,#22178,.F.);
#31753=ORIENTED_EDGE('',*,*,#22179,.F.);
#31754=ORIENTED_EDGE('',*,*,#22200,.F.);
#31755=ORIENTED_EDGE('',*,*,#22191,.F.);
#31756=ORIENTED_EDGE('',*,*,#22189,.F.);
#31757=ORIENTED_EDGE('',*,*,#22201,.F.);
#31758=ORIENTED_EDGE('',*,*,#22196,.F.);
#31759=ORIENTED_EDGE('',*,*,#22187,.F.);
#31760=ORIENTED_EDGE('',*,*,#22202,.F.);
#31761=ORIENTED_EDGE('',*,*,#22203,.F.);
#31762=ORIENTED_EDGE('',*,*,#22185,.F.);
#31763=ORIENTED_EDGE('',*,*,#22204,.F.);
#31764=ORIENTED_EDGE('',*,*,#22205,.F.);
#31765=ORIENTED_EDGE('',*,*,#22183,.F.);
#31766=ORIENTED_EDGE('',*,*,#22206,.F.);
#31767=ORIENTED_EDGE('',*,*,#22207,.F.);
#31768=ORIENTED_EDGE('',*,*,#22181,.F.);
#31769=ORIENTED_EDGE('',*,*,#22195,.F.);
#31770=ORIENTED_EDGE('',*,*,#22208,.F.);
#31771=ORIENTED_EDGE('',*,*,#22188,.F.);
#31772=ORIENTED_EDGE('',*,*,#22203,.T.);
#31773=ORIENTED_EDGE('',*,*,#22209,.T.);
#31774=ORIENTED_EDGE('',*,*,#22210,.T.);
#31775=ORIENTED_EDGE('',*,*,#22211,.T.);
#31776=ORIENTED_EDGE('',*,*,#22201,.T.);
#31777=ORIENTED_EDGE('',*,*,#22176,.F.);
#31778=ORIENTED_EDGE('',*,*,#22212,.T.);
#31779=ORIENTED_EDGE('',*,*,#22213,.F.);
#31780=ORIENTED_EDGE('',*,*,#22214,.F.);
#31781=ORIENTED_EDGE('',*,*,#22215,.F.);
#31782=ORIENTED_EDGE('',*,*,#22216,.F.);
#31783=ORIENTED_EDGE('',*,*,#22217,.F.);
#31784=ORIENTED_EDGE('',*,*,#22218,.F.);
#31785=ORIENTED_EDGE('',*,*,#22219,.F.);
#31786=ORIENTED_EDGE('',*,*,#22220,.F.);
#31787=ORIENTED_EDGE('',*,*,#22221,.F.);
#31788=ORIENTED_EDGE('',*,*,#22220,.T.);
#31789=ORIENTED_EDGE('',*,*,#22222,.T.);
#31790=ORIENTED_EDGE('',*,*,#22215,.T.);
#31791=ORIENTED_EDGE('',*,*,#22223,.T.);
#31792=ORIENTED_EDGE('',*,*,#22224,.F.);
#31793=ORIENTED_EDGE('',*,*,#22197,.F.);
#31794=ORIENTED_EDGE('',*,*,#22211,.F.);
#31795=ORIENTED_EDGE('',*,*,#22225,.F.);
#31796=ORIENTED_EDGE('',*,*,#22226,.F.);
#31797=ORIENTED_EDGE('',*,*,#22227,.F.);
#31798=ORIENTED_EDGE('',*,*,#22209,.F.);
#31799=ORIENTED_EDGE('',*,*,#22228,.F.);
#31800=ORIENTED_EDGE('',*,*,#22229,.F.);
#31801=ORIENTED_EDGE('',*,*,#22230,.F.);
#31802=ORIENTED_EDGE('',*,*,#22231,.F.);
#31803=ORIENTED_EDGE('',*,*,#22232,.F.);
#31804=ORIENTED_EDGE('',*,*,#22231,.T.);
#31805=ORIENTED_EDGE('',*,*,#22233,.T.);
#31806=ORIENTED_EDGE('',*,*,#22221,.T.);
#31807=ORIENTED_EDGE('',*,*,#22234,.T.);
#31808=ORIENTED_EDGE('',*,*,#22235,.F.);
#31809=ORIENTED_EDGE('',*,*,#22192,.F.);
#31810=ORIENTED_EDGE('',*,*,#22199,.F.);
#31811=ORIENTED_EDGE('',*,*,#22236,.F.);
#31812=ORIENTED_EDGE('',*,*,#22237,.F.);
#31813=ORIENTED_EDGE('',*,*,#22238,.F.);
#31814=ORIENTED_EDGE('',*,*,#22226,.T.);
#31815=ORIENTED_EDGE('',*,*,#22239,.T.);
#31816=ORIENTED_EDGE('',*,*,#22237,.T.);
#31817=ORIENTED_EDGE('',*,*,#22240,.T.);
#31818=ORIENTED_EDGE('',*,*,#22241,.F.);
#31819=ORIENTED_EDGE('',*,*,#22242,.F.);
#31820=ORIENTED_EDGE('',*,*,#22243,.F.);
#31821=ORIENTED_EDGE('',*,*,#22244,.F.);
#31822=ORIENTED_EDGE('',*,*,#22245,.F.);
#31823=ORIENTED_EDGE('',*,*,#22194,.F.);
#31824=ORIENTED_EDGE('',*,*,#22246,.F.);
#31825=ORIENTED_EDGE('',*,*,#22247,.F.);
#31826=ORIENTED_EDGE('',*,*,#22248,.F.);
#31827=ORIENTED_EDGE('',*,*,#22182,.F.);
#31828=ORIENTED_EDGE('',*,*,#22208,.T.);
#31829=ORIENTED_EDGE('',*,*,#22245,.T.);
#31830=ORIENTED_EDGE('',*,*,#22249,.T.);
#31831=ORIENTED_EDGE('',*,*,#22247,.T.);
#31832=ORIENTED_EDGE('',*,*,#22206,.T.);
#31833=ORIENTED_EDGE('',*,*,#22248,.T.);
#31834=ORIENTED_EDGE('',*,*,#22250,.T.);
#31835=ORIENTED_EDGE('',*,*,#22238,.T.);
#31836=ORIENTED_EDGE('',*,*,#22251,.T.);
#31837=ORIENTED_EDGE('',*,*,#22184,.F.);
#31838=ORIENTED_EDGE('',*,*,#22207,.T.);
#31839=ORIENTED_EDGE('',*,*,#22246,.T.);
#31840=ORIENTED_EDGE('',*,*,#22252,.T.);
#31841=ORIENTED_EDGE('',*,*,#22242,.T.);
#31842=ORIENTED_EDGE('',*,*,#22204,.T.);
#31843=ORIENTED_EDGE('',*,*,#22244,.T.);
#31844=ORIENTED_EDGE('',*,*,#22253,.T.);
#31845=ORIENTED_EDGE('',*,*,#22230,.T.);
#31846=ORIENTED_EDGE('',*,*,#22254,.T.);
#31847=ORIENTED_EDGE('',*,*,#22243,.T.);
#31848=ORIENTED_EDGE('',*,*,#22255,.T.);
#31849=ORIENTED_EDGE('',*,*,#22225,.T.);
#31850=ORIENTED_EDGE('',*,*,#22256,.T.);
#31851=ORIENTED_EDGE('',*,*,#22186,.F.);
#31852=ORIENTED_EDGE('',*,*,#22205,.T.);
#31853=ORIENTED_EDGE('',*,*,#22241,.T.);
#31854=ORIENTED_EDGE('',*,*,#22257,.T.);
#31855=ORIENTED_EDGE('',*,*,#22228,.T.);
#31856=ORIENTED_EDGE('',*,*,#22202,.T.);
#31857=ORIENTED_EDGE('',*,*,#22236,.T.);
#31858=ORIENTED_EDGE('',*,*,#22258,.T.);
#31859=ORIENTED_EDGE('',*,*,#22232,.T.);
#31860=ORIENTED_EDGE('',*,*,#22259,.T.);
#31861=ORIENTED_EDGE('',*,*,#22235,.T.);
#31862=ORIENTED_EDGE('',*,*,#22260,.T.);
#31863=ORIENTED_EDGE('',*,*,#22219,.T.);
#31864=ORIENTED_EDGE('',*,*,#22261,.T.);
#31865=ORIENTED_EDGE('',*,*,#22229,.T.);
#31866=ORIENTED_EDGE('',*,*,#22262,.T.);
#31867=ORIENTED_EDGE('',*,*,#22216,.T.);
#31868=ORIENTED_EDGE('',*,*,#22263,.T.);
#31869=ORIENTED_EDGE('',*,*,#22217,.T.);
#31870=ORIENTED_EDGE('',*,*,#22264,.T.);
#31871=ORIENTED_EDGE('',*,*,#22227,.T.);
#31872=ORIENTED_EDGE('',*,*,#22265,.T.);
#31873=ORIENTED_EDGE('',*,*,#22224,.T.);
#31874=ORIENTED_EDGE('',*,*,#22266,.T.);
#31875=ORIENTED_EDGE('',*,*,#22213,.T.);
#31876=ORIENTED_EDGE('',*,*,#22267,.T.);
#31877=ORIENTED_EDGE('',*,*,#22214,.T.);
#31878=ORIENTED_EDGE('',*,*,#22268,.T.);
#31879=ORIENTED_EDGE('',*,*,#22218,.T.);
#31880=ORIENTED_EDGE('',*,*,#22269,.T.);
#31881=ORIENTED_EDGE('',*,*,#22239,.F.);
#31882=ORIENTED_EDGE('',*,*,#22255,.F.);
#31883=ORIENTED_EDGE('',*,*,#22252,.F.);
#31884=ORIENTED_EDGE('',*,*,#22251,.F.);
#31885=ORIENTED_EDGE('',*,*,#22240,.F.);
#31886=ORIENTED_EDGE('',*,*,#22259,.F.);
#31887=ORIENTED_EDGE('',*,*,#22234,.F.);
#31888=ORIENTED_EDGE('',*,*,#22223,.F.);
#31889=ORIENTED_EDGE('',*,*,#22269,.F.);
#31890=ORIENTED_EDGE('',*,*,#22265,.F.);
#31891=ORIENTED_EDGE('',*,*,#22270,.T.);
#31892=ORIENTED_EDGE('',*,*,#22249,.F.);
#31893=ORIENTED_EDGE('',*,*,#22254,.F.);
#31894=ORIENTED_EDGE('',*,*,#22258,.F.);
#31895=ORIENTED_EDGE('',*,*,#22250,.F.);
#31896=ORIENTED_EDGE('',*,*,#22193,.F.);
#31897=ORIENTED_EDGE('',*,*,#22261,.F.);
#31898=ORIENTED_EDGE('',*,*,#22233,.F.);
#31899=ORIENTED_EDGE('',*,*,#22253,.F.);
#31900=ORIENTED_EDGE('',*,*,#22256,.F.);
#31901=ORIENTED_EDGE('',*,*,#22264,.F.);
#31902=ORIENTED_EDGE('',*,*,#22262,.F.);
#31903=ORIENTED_EDGE('',*,*,#22257,.F.);
#31904=ORIENTED_EDGE('',*,*,#22198,.F.);
#31905=ORIENTED_EDGE('',*,*,#22267,.F.);
#31906=ORIENTED_EDGE('',*,*,#22222,.F.);
#31907=ORIENTED_EDGE('',*,*,#22260,.F.);
#31908=ORIENTED_EDGE('',*,*,#22263,.F.);
#31909=ORIENTED_EDGE('',*,*,#22268,.F.);
#31910=ORIENTED_EDGE('',*,*,#22266,.F.);
#31911=ORIENTED_EDGE('',*,*,#22210,.F.);
#31912=ORIENTED_EDGE('',*,*,#22271,.F.);
#31913=ORIENTED_EDGE('',*,*,#22272,.T.);
#31914=ORIENTED_EDGE('',*,*,#22212,.F.);
#31915=ORIENTED_EDGE('',*,*,#22272,.F.);
#31916=ORIENTED_EDGE('',*,*,#22273,.F.);
#31917=ORIENTED_EDGE('',*,*,#22270,.F.);
#31918=ORIENTED_EDGE('',*,*,#22274,.T.);
#31919=ORIENTED_EDGE('',*,*,#22275,.T.);
#31920=ORIENTED_EDGE('',*,*,#22274,.F.);
#31921=ORIENTED_EDGE('',*,*,#22275,.F.);
#31922=ORIENTED_EDGE('',*,*,#22276,.T.);
#31923=ORIENTED_EDGE('',*,*,#22271,.T.);
#31924=ORIENTED_EDGE('',*,*,#22277,.T.);
#31925=ORIENTED_EDGE('',*,*,#22276,.F.);
#31926=ORIENTED_EDGE('',*,*,#22277,.F.);
#31927=ORIENTED_EDGE('',*,*,#22273,.T.);
#32104=CONICAL_SURFACE('',#37584,8.9203817394342,1.28983554566649);
#32105=CONICAL_SURFACE('',#37592,10.15,1.00887476453808);
#32106=CONICAL_SURFACE('',#37593,10.15,1.00887476453808);
#32107=CONICAL_SURFACE('',#37594,10.15,1.00887476453808);
#32108=CONICAL_SURFACE('',#37595,10.15,1.00887476453808);
#32109=CONICAL_SURFACE('',#37596,10.15,1.00887476453808);
#32110=CONICAL_SURFACE('',#37597,10.15,1.00887476453808);
#32111=CONICAL_SURFACE('',#37632,6.8,0.785398163397449);
#32112=CONICAL_SURFACE('',#37635,8.35,0.52183427981441);
#34159=ADVANCED_FACE('',(#5185),#32104,.T.);
#34160=ADVANCED_FACE('',(#5186),#289,.T.);
#34161=ADVANCED_FACE('',(#5187),#290,.T.);
#34162=ADVANCED_FACE('',(#5188),#32105,.T.);
#34163=ADVANCED_FACE('',(#5189),#32106,.T.);
#34164=ADVANCED_FACE('',(#5190),#32107,.T.);
#34165=ADVANCED_FACE('',(#5191),#32108,.T.);
#34166=ADVANCED_FACE('',(#5192),#32109,.T.);
#34167=ADVANCED_FACE('',(#5193),#32110,.T.);
#34168=ADVANCED_FACE('',(#5194),#291,.T.);
#34169=ADVANCED_FACE('',(#5195,#1332),#2959,.T.);
#34170=ADVANCED_FACE('',(#5196),#2960,.T.);
#34171=ADVANCED_FACE('',(#5197),#2961,.T.);
#34172=ADVANCED_FACE('',(#5198),#2962,.T.);
#34173=ADVANCED_FACE('',(#5199),#2963,.T.);
#34174=ADVANCED_FACE('',(#5200),#2964,.T.);
#34175=ADVANCED_FACE('',(#5201),#2965,.T.);
#34176=ADVANCED_FACE('',(#5202),#2966,.T.);
#34177=ADVANCED_FACE('',(#5203),#2967,.T.);
#34178=ADVANCED_FACE('',(#5204),#2968,.T.);
#34179=ADVANCED_FACE('',(#5205),#2969,.T.);
#34180=ADVANCED_FACE('',(#5206),#2970,.T.);
#34181=ADVANCED_FACE('',(#5207),#2971,.T.);
#34182=ADVANCED_FACE('',(#5208),#2972,.T.);
#34183=ADVANCED_FACE('',(#5209),#2973,.T.);
#34184=ADVANCED_FACE('',(#5210),#2974,.T.);
#34185=ADVANCED_FACE('',(#5211),#292,.T.);
#34186=ADVANCED_FACE('',(#5212),#2975,.T.);
#34187=ADVANCED_FACE('',(#5213),#293,.T.);
#34188=ADVANCED_FACE('',(#5214),#2976,.T.);
#34189=ADVANCED_FACE('',(#5215),#2977,.T.);
#34190=ADVANCED_FACE('',(#5216),#294,.T.);
#34191=ADVANCED_FACE('',(#5217),#2978,.T.);
#34192=ADVANCED_FACE('',(#5218),#2979,.T.);
#34193=ADVANCED_FACE('',(#5219),#2980,.T.);
#34194=ADVANCED_FACE('',(#5220),#2981,.T.);
#34195=ADVANCED_FACE('',(#5221),#2982,.T.);
#34196=ADVANCED_FACE('',(#5222),#2983,.T.);
#34197=ADVANCED_FACE('',(#5223),#2984,.T.);
#34198=ADVANCED_FACE('',(#5224,#1333),#2985,.F.);
#34199=ADVANCED_FACE('',(#5225),#2986,.T.);
#34200=ADVANCED_FACE('',(#5226),#2987,.T.);
#34201=ADVANCED_FACE('',(#5227),#2988,.T.);
#34202=ADVANCED_FACE('',(#5228),#2989,.T.);
#34203=ADVANCED_FACE('',(#5229),#2990,.T.);
#34204=ADVANCED_FACE('',(#5230),#32111,.F.);
#34205=ADVANCED_FACE('',(#5231),#32112,.T.);
#34206=ADVANCED_FACE('',(#5232,#1334),#2991,.T.);
#34207=ADVANCED_FACE('',(#5233),#3138,.F.);
#34220=CLOSED_SHELL('',(#34159,#34160,#34161,#34162,#34163,#34164,#34165,
#34166,#34167,#34168,#34169,#34170,#34171,#34172,#34173,#34174,#34175,#34176,
#34177,#34178,#34179,#34180,#34181,#34182,#34183,#34184,#34185,#34186,#34187,
#34188,#34189,#34190,#34191,#34192,#34193,#34194,#34195,#34196,#34197,#34198,
#34199,#34200,#34201,#34202,#34203,#34204,#34205,#34206,#34207));
#37583=AXIS2_PLACEMENT_3D('',#70878,#47095,#47096);
#37584=AXIS2_PLACEMENT_3D('',#70879,#47097,#47098);
#37585=AXIS2_PLACEMENT_3D('',#70881,#47099,#47100);
#37586=AXIS2_PLACEMENT_3D('',#70905,#47102,#47103);
#37587=AXIS2_PLACEMENT_3D('',#70945,#47104,#47105);
#37588=AXIS2_PLACEMENT_3D('',#70991,#47106,#47107);
#37589=AXIS2_PLACEMENT_3D('',#71031,#47108,#47109);
#37590=AXIS2_PLACEMENT_3D('',#71071,#47110,#47111);
#37591=AXIS2_PLACEMENT_3D('',#71117,#47112,#47113);
#37592=AXIS2_PLACEMENT_3D('',#71244,#47114,#47115);
#37593=AXIS2_PLACEMENT_3D('',#71245,#47116,#47117);
#37594=AXIS2_PLACEMENT_3D('',#71250,#47118,#47119);
#37595=AXIS2_PLACEMENT_3D('',#71260,#47120,#47121);
#37596=AXIS2_PLACEMENT_3D('',#71270,#47122,#47123);
#37597=AXIS2_PLACEMENT_3D('',#71280,#47124,#47125);
#37598=AXIS2_PLACEMENT_3D('',#71329,#47126,#47127);
#37599=AXIS2_PLACEMENT_3D('',#71331,#47128,#47129);
#37600=AXIS2_PLACEMENT_3D('',#71332,#47130,#47131);
#37601=AXIS2_PLACEMENT_3D('',#71339,#47135,#47136);
#37602=AXIS2_PLACEMENT_3D('',#71346,#47140,#47141);
#37603=AXIS2_PLACEMENT_3D('',#71353,#47145,#47146);
#37604=AXIS2_PLACEMENT_3D('',#71356,#47149,#47150);
#37605=AXIS2_PLACEMENT_3D('',#71358,#47152,#47153);
#37606=AXIS2_PLACEMENT_3D('',#71365,#47157,#47158);
#37607=AXIS2_PLACEMENT_3D('',#71374,#47160,#47161);
#37608=AXIS2_PLACEMENT_3D('',#71381,#47165,#47166);
#37609=AXIS2_PLACEMENT_3D('',#71384,#47169,#47170);
#37610=AXIS2_PLACEMENT_3D('',#71386,#47172,#47173);
#37611=AXIS2_PLACEMENT_3D('',#71393,#47177,#47178);
#37612=AXIS2_PLACEMENT_3D('',#71396,#47181,#47182);
#37613=AXIS2_PLACEMENT_3D('',#71412,#47184,#47185);
#37614=AXIS2_PLACEMENT_3D('',#71421,#47187,#47188);
#37615=AXIS2_PLACEMENT_3D('',#71467,#47190,#47191);
#37616=AXIS2_PLACEMENT_3D('',#71500,#47194,#47195);
#37617=AXIS2_PLACEMENT_3D('',#71503,#47198,#47199);
#37618=AXIS2_PLACEMENT_3D('',#71536,#47202,#47203);
#37619=AXIS2_PLACEMENT_3D('',#71539,#47206,#47207);
#37620=AXIS2_PLACEMENT_3D('',#71542,#47210,#47211);
#37621=AXIS2_PLACEMENT_3D('',#71545,#47214,#47215);
#37622=AXIS2_PLACEMENT_3D('',#71548,#47218,#47219);
#37623=AXIS2_PLACEMENT_3D('',#71551,#47222,#47223);
#37624=AXIS2_PLACEMENT_3D('',#71554,#47226,#47227);
#37625=AXIS2_PLACEMENT_3D('',#71555,#47228,#47229);
#37626=AXIS2_PLACEMENT_3D('',#71557,#47230,#47231);
#37627=AXIS2_PLACEMENT_3D('',#71558,#47232,#47233);
#37628=AXIS2_PLACEMENT_3D('',#71559,#47234,#47235);
#37629=AXIS2_PLACEMENT_3D('',#71560,#47236,#47237);
#37630=AXIS2_PLACEMENT_3D('',#71561,#47238,#47239);
#37631=AXIS2_PLACEMENT_3D('',#71562,#47240,#47241);
#37632=AXIS2_PLACEMENT_3D('',#71563,#47242,#47243);
#37633=AXIS2_PLACEMENT_3D('',#71566,#47244,#47245);
#37634=AXIS2_PLACEMENT_3D('',#71568,#47247,#47248);
#37635=AXIS2_PLACEMENT_3D('',#71569,#47249,#47250);
#37636=AXIS2_PLACEMENT_3D('',#71572,#47252,#47253);
#37637=AXIS2_PLACEMENT_3D('',#71573,#47254,#47255);
#37638=AXIS2_PLACEMENT_3D('',#71575,#47256,#47257);
#37639=AXIS2_PLACEMENT_3D('',#71576,#47258,#47259);
#47095=DIRECTION('axis',(0.,0.,1.));
#47096=DIRECTION('refdir',(1.,0.,0.));
#47097=DIRECTION('center_axis',(-1.,0.,-2.15639575486977E-15));
#47098=DIRECTION('ref_axis',(0.,1.,3.2200311221276E-17));
#47099=DIRECTION('center_axis',(-1.,0.,0.));
#47100=DIRECTION('ref_axis',(0.,1.,0.));
#47101=DIRECTION('',(-0.277278884798545,-0.960789477484467,-7.46523506113315E-16));
#47102=DIRECTION('center_axis',(1.,0.,0.));
#47103=DIRECTION('ref_axis',(0.,1.,6.12323399573676E-17));
#47104=DIRECTION('center_axis',(1.,0.,0.));
#47105=DIRECTION('ref_axis',(0.,1.,6.12323399573676E-17));
#47106=DIRECTION('center_axis',(1.,0.,0.));
#47107=DIRECTION('ref_axis',(0.,1.,6.12323399573676E-17));
#47108=DIRECTION('center_axis',(1.,0.,0.));
#47109=DIRECTION('ref_axis',(0.,1.,6.12323399573676E-17));
#47110=DIRECTION('center_axis',(1.,0.,0.));
#47111=DIRECTION('ref_axis',(0.,1.,6.12323399573676E-17));
#47112=DIRECTION('center_axis',(1.,0.,0.));
#47113=DIRECTION('ref_axis',(0.,1.,6.12323399573676E-17));
#47114=DIRECTION('center_axis',(-1.,0.,0.));
#47115=DIRECTION('ref_axis',(0.,1.,0.));
#47116=DIRECTION('center_axis',(-1.,0.,0.));
#47117=DIRECTION('ref_axis',(0.,1.,0.));
#47118=DIRECTION('center_axis',(-1.,0.,0.));
#47119=DIRECTION('ref_axis',(0.,1.,0.));
#47120=DIRECTION('center_axis',(-1.,0.,0.));
#47121=DIRECTION('ref_axis',(0.,1.,0.));
#47122=DIRECTION('center_axis',(-1.,0.,0.));
#47123=DIRECTION('ref_axis',(0.,1.,0.));
#47124=DIRECTION('center_axis',(-1.,0.,0.));
#47125=DIRECTION('ref_axis',(0.,1.,0.));
#47126=DIRECTION('center_axis',(1.,0.,0.));
#47127=DIRECTION('ref_axis',(0.,0.,-1.));
#47128=DIRECTION('center_axis',(-1.,0.,0.));
#47129=DIRECTION('ref_axis',(0.,1.,0.));
#47130=DIRECTION('center_axis',(-0.547750005235851,-0.724553275351849,0.418321028566617));
#47131=DIRECTION('ref_axis',(0.606949534647158,0.,0.79474037420506));
#47132=DIRECTION('',(0.,-0.5,-0.866025403784439));
#47133=DIRECTION('',(0.677497944020808,-0.0907675134870585,0.729902592366238));
#47134=DIRECTION('',(-0.677497944020809,0.67749794402081,0.286344323664976));
#47135=DIRECTION('center_axis',(-0.547750005235851,0.,0.836642057133231));
#47136=DIRECTION('ref_axis',(0.836642057133231,0.,0.547750005235851));
#47137=DIRECTION('',(0.,-1.,0.));
#47138=DIRECTION('',(0.67749794402081,0.586730430533746,0.443558268701261));
#47139=DIRECTION('',(-0.677497944020808,0.58673043053375,-0.443558268701259));
#47140=DIRECTION('center_axis',(-0.547750005235851,-0.72455327535185,-0.418321028566616));
#47141=DIRECTION('ref_axis',(-0.606949534647158,0.,0.79474037420506));
#47142=DIRECTION('',(0.,0.499999999999999,-0.866025403784439));
#47143=DIRECTION('',(0.677497944020809,-0.677497944020809,0.286344323664978));
#47144=DIRECTION('',(-0.67749794402081,0.0907675134870618,0.729902592366236));
#47145=DIRECTION('center_axis',(-0.707106781186548,-0.707106781186547,0.));
#47146=DIRECTION('ref_axis',(0.,0.,1.));
#47147=DIRECTION('',(0.,0.,1.));
#47148=DIRECTION('',(0.,0.,-1.));
#47149=DIRECTION('center_axis',(0.353397121838513,-0.810143725338629,0.467736697908881));
#47150=DIRECTION('ref_axis',(0.797870555551687,0.,-0.602828812005234));
#47151=DIRECTION('',(2.56395024851141E-15,0.5,0.866025403784439));
#47152=DIRECTION('center_axis',(-0.547750005235851,0.72455327535185,0.418321028566616));
#47153=DIRECTION('ref_axis',(0.606949534647158,0.,0.79474037420506));
#47154=DIRECTION('',(0.,-0.500000000000001,0.866025403784438));
#47155=DIRECTION('',(0.677497944020809,0.677497944020809,-0.286344323664978));
#47156=DIRECTION('',(-0.677497944020809,-0.0907675134870602,-0.729902592366237));
#47157=DIRECTION('center_axis',(0.353397121838516,2.02674207780683E-12,
0.935473395814255));
#47158=DIRECTION('ref_axis',(0.935473395814254,0.,-0.353397121838516));
#47159=DIRECTION('',(0.,1.,0.));
#47160=DIRECTION('center_axis',(-0.547750005235851,0.,-0.836642057133231));
#47161=DIRECTION('ref_axis',(-0.836642057133231,0.,0.547750005235851));
#47162=DIRECTION('',(0.,1.,0.));
#47163=DIRECTION('',(0.677497944020809,-0.586730430533748,-0.44355826870126));
#47164=DIRECTION('',(-0.67749794402081,-0.586730430533747,0.44355826870126));
#47165=DIRECTION('center_axis',(-0.707106781186548,-0.353553390593274,-0.612372435695794));
#47166=DIRECTION('ref_axis',(-0.654653670707977,0.,0.755928946018455));
#47167=DIRECTION('',(0.,-0.866025403784439,0.5));
#47168=DIRECTION('',(0.,0.866025403784439,-0.5));
#47169=DIRECTION('center_axis',(0.353397121838512,-0.810143725340653,-0.467736697905376));
#47170=DIRECTION('ref_axis',(-0.797870555549515,0.,-0.602828812008109));
#47171=DIRECTION('',(7.69185074553426E-15,-0.499999999999999,0.866025403784439));
#47172=DIRECTION('center_axis',(-0.547750005235851,0.72455327535185,-0.418321028566616));
#47173=DIRECTION('ref_axis',(-0.606949534647157,0.,0.79474037420506));
#47174=DIRECTION('',(0.677497944020809,0.0907675134870632,-0.729902592366237));
#47175=DIRECTION('',(-0.677497944020809,-0.677497944020809,-0.286344323664978));
#47176=DIRECTION('',(0.,0.5,0.866025403784439));
#47177=DIRECTION('center_axis',(-0.707106781186548,0.707106781186547,-2.14132276458349E-16));
#47178=DIRECTION('ref_axis',(-3.02828769509222E-16,0.,1.));
#47179=DIRECTION('',(0.,-3.02828769509223E-16,-1.));
#47180=DIRECTION('',(0.,3.02828769509223E-16,1.));
#47181=DIRECTION('center_axis',(0.353397121838516,0.810143725340652,0.467736697905373));
#47182=DIRECTION('ref_axis',(0.79787055554951,0.,-0.602828812008115));
#47183=DIRECTION('',(0.,0.500000000000001,-0.866025403784438));
#47184=DIRECTION('center_axis',(0.353397121838512,-2.0243364797534E-12,
-0.935473395814256));
#47185=DIRECTION('ref_axis',(-0.935473395814256,0.,-0.353397121838512));
#47186=DIRECTION('',(-2.56395024851142E-15,-1.,0.));
#47187=DIRECTION('center_axis',(0.353397121838513,0.810143725338629,-0.46773669790888));
#47188=DIRECTION('ref_axis',(-0.797870555551687,0.,-0.602828812005235));
#47189=DIRECTION('',(0.,-0.5,-0.866025403784439));
#47190=DIRECTION('center_axis',(0.,0.866025403784439,-0.5));
#47191=DIRECTION('ref_axis',(-1.,0.,0.));
#47192=DIRECTION('',(-1.,0.,0.));
#47193=DIRECTION('',(1.,0.,0.));
#47194=DIRECTION('center_axis',(0.,0.,-1.));
#47195=DIRECTION('ref_axis',(-1.,0.,0.));
#47196=DIRECTION('',(-1.,0.,0.));
#47197=DIRECTION('',(1.,0.,0.));
#47198=DIRECTION('center_axis',(0.,0.866025403784438,0.500000000000001));
#47199=DIRECTION('ref_axis',(1.,0.,0.));
#47200=DIRECTION('',(-1.,0.,0.));
#47201=DIRECTION('',(1.,0.,0.));
#47202=DIRECTION('center_axis',(-0.707106781186547,0.353553390593274,-0.612372435695795));
#47203=DIRECTION('ref_axis',(-0.654653670707977,0.,0.755928946018454));
#47204=DIRECTION('',(0.,-0.866025403784439,-0.5));
#47205=DIRECTION('',(0.,0.866025403784439,0.5));
#47206=DIRECTION('center_axis',(0.,-0.866025403784439,-0.499999999999999));
#47207=DIRECTION('ref_axis',(0.,0.499999999999999,-0.866025403784439));
#47208=DIRECTION('',(-1.,0.,0.));
#47209=DIRECTION('',(1.,0.,0.));
#47210=DIRECTION('center_axis',(0.,0.,1.));
#47211=DIRECTION('ref_axis',(1.,0.,0.));
#47212=DIRECTION('',(-1.,0.,0.));
#47213=DIRECTION('',(1.,0.,0.));
#47214=DIRECTION('center_axis',(-0.707106781186548,0.353553390593274,0.612372435695794));
#47215=DIRECTION('ref_axis',(0.654653670707977,0.,0.755928946018455));
#47216=DIRECTION('',(0.,0.866025403784439,-0.5));
#47217=DIRECTION('',(0.,-0.866025403784439,0.5));
#47218=DIRECTION('center_axis',(0.,-0.866025403784439,0.5));
#47219=DIRECTION('ref_axis',(1.,0.,0.));
#47220=DIRECTION('',(-1.,0.,0.));
#47221=DIRECTION('',(1.,0.,0.));
#47222=DIRECTION('center_axis',(-0.707106781186548,-0.353553390593273,0.612372435695794));
#47223=DIRECTION('ref_axis',(0.654653670707976,0.,0.755928946018455));
#47224=DIRECTION('',(0.,0.866025403784439,0.5));
#47225=DIRECTION('',(0.,-0.866025403784439,-0.5));
#47226=DIRECTION('center_axis',(0.,1.,-3.02828769509223E-16));
#47227=DIRECTION('ref_axis',(0.,3.02828769509223E-16,1.));
#47228=DIRECTION('center_axis',(1.,0.,0.));
#47229=DIRECTION('ref_axis',(0.,0.,-1.));
#47230=DIRECTION('center_axis',(1.,0.,0.));
#47231=DIRECTION('ref_axis',(0.,1.,0.));
#47232=DIRECTION('center_axis',(0.,0.5,-0.866025403784439));
#47233=DIRECTION('ref_axis',(0.,0.866025403784439,0.5));
#47234=DIRECTION('center_axis',(0.,-0.5,-0.866025403784439));
#47235=DIRECTION('ref_axis',(0.,0.866025403784439,-0.5));
#47236=DIRECTION('center_axis',(0.,0.5,0.866025403784439));
#47237=DIRECTION('ref_axis',(0.,-0.866025403784439,0.5));
#47238=DIRECTION('center_axis',(0.,-1.,0.));
#47239=DIRECTION('ref_axis',(0.,0.,-1.));
#47240=DIRECTION('center_axis',(0.,-0.5,0.866025403784439));
#47241=DIRECTION('ref_axis',(0.,-0.866025403784439,-0.5));
#47242=DIRECTION('center_axis',(1.,0.,0.));
#47243=DIRECTION('ref_axis',(0.,1.,0.));
#47244=DIRECTION('center_axis',(1.,0.,0.));
#47245=DIRECTION('ref_axis',(0.,0.,-1.));
#47246=DIRECTION('',(0.707106781186547,-0.707106781186548,-8.65956056235494E-17));
#47247=DIRECTION('center_axis',(1.,0.,0.));
#47248=DIRECTION('ref_axis',(0.,0.,-1.));
#47249=DIRECTION('center_axis',(1.,0.,0.));
#47250=DIRECTION('ref_axis',(0.,1.,0.));
#47251=DIRECTION('',(-0.866906303057535,0.498471124258083,6.10451066790044E-17));
#47252=DIRECTION('center_axis',(1.,0.,0.));
#47253=DIRECTION('ref_axis',(0.,0.,-1.));
#47254=DIRECTION('center_axis',(-1.,0.,0.));
#47255=DIRECTION('ref_axis',(0.,0.,1.));
#47256=DIRECTION('center_axis',(1.,0.,0.));
#47257=DIRECTION('ref_axis',(0.,0.,-1.));
#47258=DIRECTION('center_axis',(1.,0.,0.));
#47259=DIRECTION('ref_axis',(0.,0.,-1.));
#47260=DIRECTION('',(-1.,0.,0.));
#70878=CARTESIAN_POINT('',(0.,0.,0.));
#70879=CARTESIAN_POINT('Origin',(14.1667966825785,0.,-2.87239068222369E-16));
#70880=CARTESIAN_POINT('',(14.3,-8.45882352941176,1.03590711598464E-15));
#70881=CARTESIAN_POINT('Origin',(14.3,0.,0.));
#70882=CARTESIAN_POINT('',(14.0966872156073,-9.1646003104954,-0.000235982960761385));
#70883=CARTESIAN_POINT('',(14.1667966825785,-8.9203817394342,-1.6669098308818E-15));
#70884=CARTESIAN_POINT('',(14.0358618182521,-9.09714729409388,-2.2913561246914));
#70885=CARTESIAN_POINT('Ctrl Pts',(14.0966872156073,-9.1646003104954,-0.000235982960761354));
#70886=CARTESIAN_POINT('Ctrl Pts',(14.096667975927,-9.16460269692416,-0.0788499963175328));
#70887=CARTESIAN_POINT('Ctrl Pts',(14.0964337489381,-9.16436435538848,-0.157458304901251));
#70888=CARTESIAN_POINT('Ctrl Pts',(14.0959893606634,-9.16388490893575,-0.23607213292966));
#70889=CARTESIAN_POINT('Ctrl Pts',(14.0951146780166,-9.16294122181289,-0.390806528744216));
#70890=CARTESIAN_POINT('Ctrl Pts',(14.0934278040135,-9.16106393006443,-0.545363216810532));
#70891=CARTESIAN_POINT('Ctrl Pts',(14.0909765857551,-9.15825881192215,-0.699825257957074));
#70892=CARTESIAN_POINT('Ctrl Pts',(14.0891704149768,-9.15619187137072,-0.813640020939149));
#70893=CARTESIAN_POINT('Ctrl Pts',(14.0869493584505,-9.15362107196599,-0.927403243780337));
#70894=CARTESIAN_POINT('Ctrl Pts',(14.0842873855616,-9.15055006079841,-1.04117270406207));
#70895=CARTESIAN_POINT('Ctrl Pts',(14.0808085904244,-9.14653671462165,-1.1898521466101));
#70896=CARTESIAN_POINT('Ctrl Pts',(14.0765836260547,-9.14167463053302,-1.33830456859723));
#70897=CARTESIAN_POINT('Ctrl Pts',(14.0715649306596,-9.1359838442516,-1.48668516439165));
#70898=CARTESIAN_POINT('Ctrl Pts',(14.0667384825238,-9.13051105049219,-1.62938186015989));
#70899=CARTESIAN_POINT('Ctrl Pts',(14.0611778355173,-9.12427176256957,-1.77201223274345));
#70900=CARTESIAN_POINT('Ctrl Pts',(14.0548601236482,-9.11728218271552,-1.91467104387642));
#70901=CARTESIAN_POINT('Ctrl Pts',(14.0493110055173,-9.11114293402874,-2.0399744150652));
#70902=CARTESIAN_POINT('Ctrl Pts',(14.0431780217821,-9.10442480241651,-2.16529922277692));
#70903=CARTESIAN_POINT('Ctrl Pts',(14.0364597916687,-9.0971382152186,-2.29067954584981));
#70904=CARTESIAN_POINT('',(14.0346021788821,-6.53571152371397,-6.73113542385575));
#70905=CARTESIAN_POINT('Origin',(14.0335933651569,0.,-5.74478136444738E-16));
#70906=CARTESIAN_POINT('',(14.0357899498044,-2.56414768532747,-9.02407043229182));
#70907=CARTESIAN_POINT('Ctrl Pts',(14.0346021788821,-6.53571152371397,-6.73113542385575));
#70908=CARTESIAN_POINT('Ctrl Pts',(14.037490920202,-6.49086101686042,-6.76062130272172));
#70909=CARTESIAN_POINT('Ctrl Pts',(14.0402815726799,-6.44595104664353,-6.79002177619354));
#70910=CARTESIAN_POINT('Ctrl Pts',(14.0429752481594,-6.40097722143761,-6.81933831082405));
#70911=CARTESIAN_POINT('Ctrl Pts',(14.0504757625031,-6.27574802303614,-6.90096992910151));
#70912=CARTESIAN_POINT('Ctrl Pts',(14.0572232832294,-6.15002692231759,-6.98194901081926));
#70913=CARTESIAN_POINT('Ctrl Pts',(14.0631875076052,-6.02378040933136,-7.06227499667437));
#70914=CARTESIAN_POINT('Ctrl Pts',(14.0670738259238,-5.94151755247907,-7.11461580926091));
#70915=CARTESIAN_POINT('Ctrl Pts',(14.0706279215876,-5.85903066199963,-7.16667984778686));
#70916=CARTESIAN_POINT('Ctrl Pts',(14.0738450240434,-5.77630052750431,-7.21847226290525));
#70917=CARTESIAN_POINT('Ctrl Pts',(14.0791867260652,-5.63893476661847,-7.30446879312068));
#70918=CARTESIAN_POINT('Ctrl Pts',(14.0835906402011,-5.50109523148508,-7.38959315710351));
#70919=CARTESIAN_POINT('Ctrl Pts',(14.0870443139107,-5.36272714628941,-7.47386405825115));
#70920=CARTESIAN_POINT('Ctrl Pts',(14.0900251718151,-5.24330196743517,-7.54659808089469));
#70921=CARTESIAN_POINT('Ctrl Pts',(14.0922987244798,-5.12348189405599,-7.61869696507324));
#70922=CARTESIAN_POINT('Ctrl Pts',(14.0938730282238,-5.0032076555115,-7.6901839122321));
#70923=CARTESIAN_POINT('Ctrl Pts',(14.0960271700124,-4.83863473600432,-7.78800049991507));
#70924=CARTESIAN_POINT('Ctrl Pts',(14.0968652699818,-4.67348773079844,-7.8845083580373));
#70925=CARTESIAN_POINT('Ctrl Pts',(14.0964383665758,-4.5076387644692,-7.97977606599508));
#70926=CARTESIAN_POINT('Ctrl Pts',(14.0963267565809,-4.46427906755682,-8.00468293779545));
#70927=CARTESIAN_POINT('Ctrl Pts',(14.0961289474093,-4.42087129224503,-8.02950504143431));
#70928=CARTESIAN_POINT('Ctrl Pts',(14.0958463988297,-4.37741303746945,-8.0542435417795));
#70929=CARTESIAN_POINT('Ctrl Pts',(14.094972077556,-4.24293536027673,-8.13079461546694));
#70930=CARTESIAN_POINT('Ctrl Pts',(14.0932865822815,-4.10814556901557,-8.2064478459118));
#70931=CARTESIAN_POINT('Ctrl Pts',(14.0908378720276,-3.97297486435817,-8.2812496228984));
#70932=CARTESIAN_POINT('Ctrl Pts',(14.0890335492626,-3.87337484872653,-8.3363670255636));
#70933=CARTESIAN_POINT('Ctrl Pts',(14.0868149528525,-3.77356809910472,-8.39102197337117));
#70934=CARTESIAN_POINT('Ctrl Pts',(14.0841559268849,-3.67350630415314,-8.44524657114366));
#70935=CARTESIAN_POINT('Ctrl Pts',(14.0806813229798,-3.54275349928081,-8.5161029679858));
#70936=CARTESIAN_POINT('Ctrl Pts',(14.0764615201052,-3.41177376280883,-8.58611052772029));
#70937=CARTESIAN_POINT('Ctrl Pts',(14.0714486898468,-3.28044252824194,-8.65536429918192));
#70938=CARTESIAN_POINT('Ctrl Pts',(14.0666278773627,-3.15414197096834,-8.72196528681254));
#70939=CARTESIAN_POINT('Ctrl Pts',(14.0610735151129,-3.0275162045262,-8.7878691248368));
#70940=CARTESIAN_POINT('Ctrl Pts',(14.054762506757,-2.90049109866216,-8.85313731723162));
#70941=CARTESIAN_POINT('Ctrl Pts',(14.04921748605,-2.7888834438153,-8.9104836964354));
#70942=CARTESIAN_POINT('Ctrl Pts',(14.0430885450049,-2.67696791838211,-8.96733907859069));
#70943=CARTESIAN_POINT('Ctrl Pts',(14.036374153903,-2.56472008839194,-9.02372962028732));
#70944=CARTESIAN_POINT('',(14.0357899498032,2.56414768532832,-9.02407043229137));
#70945=CARTESIAN_POINT('Origin',(14.0335933651569,0.,-5.74478136444738E-16));
#70946=CARTESIAN_POINT('',(14.0346021788821,6.53571152371399,-6.73113542385574));
#70947=CARTESIAN_POINT('Ctrl Pts',(14.036374153903,2.56472008839191,-9.02372962028734));
#70948=CARTESIAN_POINT('Ctrl Pts',(14.0439581544769,2.69150561430802,-8.96003569866473));
#70949=CARTESIAN_POINT('Ctrl Pts',(14.0507940165627,2.81788693530708,-8.89574019624407));
#70950=CARTESIAN_POINT('Ctrl Pts',(14.056887537588,2.9439106365035,-8.83079680975475));
#70951=CARTESIAN_POINT('Ctrl Pts',(14.0631313247637,3.07304208055634,-8.76425192018689));
#70952=CARTESIAN_POINT('Ctrl Pts',(14.0685958234887,3.2017981474923,-8.69702680530498));
#70953=CARTESIAN_POINT('Ctrl Pts',(14.0733090155991,3.33027166379957,-8.62904584746935));
#70954=CARTESIAN_POINT('Ctrl Pts',(14.0737328173227,3.3418237703919,-8.62293312249895));
#70955=CARTESIAN_POINT('Ctrl Pts',(14.0741505579372,3.35337361963567,-8.61681426950855));
#70956=CARTESIAN_POINT('Ctrl Pts',(14.0745622655563,3.36492129486017,-8.61068922364997));
#70957=CARTESIAN_POINT('Ctrl Pts',(14.0794394387139,3.50171743128368,-8.5381306702978));
#70958=CARTESIAN_POINT('Ctrl Pts',(14.0834615310168,3.63801904201667,-8.46480359133271));
#70959=CARTESIAN_POINT('Ctrl Pts',(14.0866814188315,3.77393577057594,-8.39063029663735));
#70960=CARTESIAN_POINT('Ctrl Pts',(14.0882552127477,3.84036818462935,-8.35437640002625));
#70961=CARTESIAN_POINT('Ctrl Pts',(14.0896378032368,3.90670926990041,-8.31791993646687));
#70962=CARTESIAN_POINT('Ctrl Pts',(14.090837669424,3.97297492845534,-8.28124971544123));
#70963=CARTESIAN_POINT('Ctrl Pts',(14.0919557958865,4.03472630304775,-8.24707761779182));
#70964=CARTESIAN_POINT('Ctrl Pts',(14.0929152942354,4.09641222151585,-8.21271986900143));
#70965=CARTESIAN_POINT('Ctrl Pts',(14.0937114070427,4.15803990964946,-8.17817121287965));
#70966=CARTESIAN_POINT('Ctrl Pts',(14.0958985068728,4.32734494406736,-8.0832583321448));
#70967=CARTESIAN_POINT('Ctrl Pts',(14.0968439958901,4.49592110849515,-7.98706849201295));
#70968=CARTESIAN_POINT('Ctrl Pts',(14.0964643580788,4.66390152286281,-7.88952765023803));
#70969=CARTESIAN_POINT('Ctrl Pts',(14.0963723250581,4.7046238758636,-7.86588148526276));
#70970=CARTESIAN_POINT('Ctrl Pts',(14.0962026412764,4.74531125568717,-7.84215584473792));
#70971=CARTESIAN_POINT('Ctrl Pts',(14.095954561874,4.78596555791062,-7.81834956722902));
#70972=CARTESIAN_POINT('Ctrl Pts',(14.0950534684957,4.9336332891507,-7.73187854702333));
#70973=CARTESIAN_POINT('Ctrl Pts',(14.0931172756095,5.08065748201068,-7.64446522212414));
#70974=CARTESIAN_POINT('Ctrl Pts',(14.0901216005508,5.22713884337462,-7.55606608075544));
#70975=CARTESIAN_POINT('Ctrl Pts',(14.0884090550303,5.31087823243389,-7.50553070872822));
#70976=CARTESIAN_POINT('Ctrl Pts',(14.0863508376835,5.39443971659127,-7.4546733264031));
#70977=CARTESIAN_POINT('Ctrl Pts',(14.0839473935999,5.47783644876651,-7.40348815992952));
#70978=CARTESIAN_POINT('Ctrl Pts',(14.0801455293264,5.60975674545584,-7.32252141014012));
#70979=CARTESIAN_POINT('Ctrl Pts',(14.0754874908681,5.74104585820764,-7.24086784135944));
#70980=CARTESIAN_POINT('Ctrl Pts',(14.0699826640698,5.87179177769892,-7.15849937346099));
#70981=CARTESIAN_POINT('Ctrl Pts',(14.0646793238266,5.99775216153913,-7.07914573953355));
#70982=CARTESIAN_POINT('Ctrl Pts',(14.0585899970415,6.12320849014782,-6.9991284498085));
#70983=CARTESIAN_POINT('Ctrl Pts',(14.0517394686096,6.2481988125042,-6.91844353123613));
#70984=CARTESIAN_POINT('Ctrl Pts',(14.0489440163948,6.2992028302131,-6.88551894205096));
#70985=CARTESIAN_POINT('Ctrl Pts',(14.046022010621,6.35012876048407,-6.85248344327514));
#70986=CARTESIAN_POINT('Ctrl Pts',(14.0429759898738,6.40097709821819,-6.81933789599594));
#70987=CARTESIAN_POINT('Ctrl Pts',(14.0402820510809,6.44594800319266,-6.79002356000301));
#70988=CARTESIAN_POINT('Ctrl Pts',(14.0374911009489,6.49085821058925,-6.76062314763669));
#70989=CARTESIAN_POINT('Ctrl Pts',(14.0346021788821,6.53571152371399,-6.73113542385574));
#70990=CARTESIAN_POINT('',(14.0346846831548,9.09718960292736,-2.29455299637842));
#70991=CARTESIAN_POINT('Origin',(14.0335933651569,0.,-5.74478136444738E-16));
#70992=CARTESIAN_POINT('',(14.035861818251,9.09714729409392,2.2913561246905));
#70993=CARTESIAN_POINT('Ctrl Pts',(14.0346846831548,9.09718960292737,-2.29455299637841));
#70994=CARTESIAN_POINT('Ctrl Pts',(14.0375755696933,9.10029985513172,-2.24096964017326));
#70995=CARTESIAN_POINT('Ctrl Pts',(14.0403683507454,9.10330641202518,-2.18737754787367));
#70996=CARTESIAN_POINT('Ctrl Pts',(14.043064127072,9.1062083478486,-2.13377218640335));
#70997=CARTESIAN_POINT('Ctrl Pts',(14.0505699144896,9.11428814036511,-1.98452002343093));
#70998=CARTESIAN_POINT('Ctrl Pts',(14.0573226099963,9.12155698997572,-1.83516862171975));
#70999=CARTESIAN_POINT('Ctrl Pts',(14.0632917846551,9.12799766353303,-1.68568903224694));
#71000=CARTESIAN_POINT('Ctrl Pts',(14.0671820861082,9.1321952558521,-1.58826841760994));
#71001=CARTESIAN_POINT('Ctrl Pts',(14.0707399396716,9.13604105522664,-1.49079227060806));
#71002=CARTESIAN_POINT('Ctrl Pts',(14.0739605337436,9.13952991576929,-1.39324130828909));
#71003=CARTESIAN_POINT('Ctrl Pts',(14.079307034207,9.1453217647546,-1.23129719065638));
#71004=CARTESIAN_POINT('Ctrl Pts',(14.0837153543481,9.15012154561387,-1.06937897158459));
#71005=CARTESIAN_POINT('Ctrl Pts',(14.0871728595391,9.15391807261198,-0.907429557799676));
#71006=CARTESIAN_POINT('Ctrl Pts',(14.0901574685142,9.15719533408425,-0.767630585075904));
#71007=CARTESIAN_POINT('Ctrl Pts',(14.0924341327935,9.15972498534993,-0.627807045688716));
#71008=CARTESIAN_POINT('Ctrl Pts',(14.0940107917454,9.16149748328792,-0.487895780218637));
#71009=CARTESIAN_POINT('Ctrl Pts',(14.0961676570875,9.16392225585315,-0.296497533254805));
#71010=CARTESIAN_POINT('Ctrl Pts',(14.0970076672682,9.16492702857341,-0.105255742388477));
#71011=CARTESIAN_POINT('Ctrl Pts',(14.0965815587046,9.16450726213935,0.0859751166229818));
#71012=CARTESIAN_POINT('Ctrl Pts',(14.096470075072,9.16439743781078,0.13600722731108));
#71013=CARTESIAN_POINT('Ctrl Pts',(14.096272189818,9.16419005072871,0.186038673928651));
#71014=CARTESIAN_POINT('Ctrl Pts',(14.0959893606634,9.16388490893575,0.236072132929773));
#71015=CARTESIAN_POINT('Ctrl Pts',(14.0951146780166,9.16294122181289,0.390806528744278));
#71016=CARTESIAN_POINT('Ctrl Pts',(14.0934278040135,9.16106393006444,0.545363216810541));
#71017=CARTESIAN_POINT('Ctrl Pts',(14.0909765857551,9.15825881192215,0.699825257957071));
#71018=CARTESIAN_POINT('Ctrl Pts',(14.0891704149768,9.15619187137072,0.813640020939152));
#71019=CARTESIAN_POINT('Ctrl Pts',(14.0869493584505,9.15362107196599,0.927403243780368));
#71020=CARTESIAN_POINT('Ctrl Pts',(14.0842873855616,9.15055006079841,1.04117270406217));
#71021=CARTESIAN_POINT('Ctrl Pts',(14.0808085904244,9.14653671462164,1.18985214661074));
#71022=CARTESIAN_POINT('Ctrl Pts',(14.0765836260547,9.14167463053298,1.33830456859842));
#71023=CARTESIAN_POINT('Ctrl Pts',(14.0715649306595,9.13598384425154,1.48668516439338));
#71024=CARTESIAN_POINT('Ctrl Pts',(14.0667384825238,9.13051105049213,1.6293818601613));
#71025=CARTESIAN_POINT('Ctrl Pts',(14.0611778355173,9.12427176256952,1.77201223274453));
#71026=CARTESIAN_POINT('Ctrl Pts',(14.0548601236482,9.11728218271549,1.91467104387717));
#71027=CARTESIAN_POINT('Ctrl Pts',(14.0493110055172,9.11114293402872,2.03997441506574));
#71028=CARTESIAN_POINT('Ctrl Pts',(14.043178021782,9.1044248024165,2.16529922277725));
#71029=CARTESIAN_POINT('Ctrl Pts',(14.0364597916687,9.0971382152186,2.29067954584992));
#71030=CARTESIAN_POINT('',(14.0346021788821,6.53571152371428,6.73113542385557));
#71031=CARTESIAN_POINT('Origin',(14.0335933651569,0.,-5.74478136444738E-16));
#71032=CARTESIAN_POINT('',(14.0357899498033,2.56414768532805,9.02407043229152));
#71033=CARTESIAN_POINT('Ctrl Pts',(14.0346021788821,6.53571152371428,6.73113542385557));
#71034=CARTESIAN_POINT('Ctrl Pts',(14.037490920202,6.49086101686062,6.76062130272161));
#71035=CARTESIAN_POINT('Ctrl Pts',(14.0402815726799,6.44595104664364,6.79002177619349));
#71036=CARTESIAN_POINT('Ctrl Pts',(14.0429752481594,6.40097722143762,6.81933831082406));
#71037=CARTESIAN_POINT('Ctrl Pts',(14.0504757625032,6.27574802303421,6.90096992910279));
#71038=CARTESIAN_POINT('Ctrl Pts',(14.0572232832295,6.15002692231372,6.98194901082178));
#71039=CARTESIAN_POINT('Ctrl Pts',(14.0631875076055,6.02378040932554,7.06227499667809));
#71040=CARTESIAN_POINT('Ctrl Pts',(14.0670738259239,5.9415175524751,7.11461580926345));
#71041=CARTESIAN_POINT('Ctrl Pts',(14.0706279215876,5.85903066199751,7.16667984778822));
#71042=CARTESIAN_POINT('Ctrl Pts',(14.0738450240434,5.77630052750406,7.21847226290544));
#71043=CARTESIAN_POINT('Ctrl Pts',(14.079186726065,5.63893476662222,7.30446879311835));
#71044=CARTESIAN_POINT('Ctrl Pts',(14.0835906402009,5.5010952314928,7.38959315709877));
#71045=CARTESIAN_POINT('Ctrl Pts',(14.0870443139104,5.3627271463011,7.47386405824405));
#71046=CARTESIAN_POINT('Ctrl Pts',(14.0900251718149,5.24330196744293,7.54659808089004));
#71047=CARTESIAN_POINT('Ctrl Pts',(14.0922987244797,5.1234818940598,7.618696965071));
#71048=CARTESIAN_POINT('Ctrl Pts',(14.0938730282238,5.00320765551131,7.69018391223224));
#71049=CARTESIAN_POINT('Ctrl Pts',(14.0960271700123,4.838634736007,7.7880004999135));
#71050=CARTESIAN_POINT('Ctrl Pts',(14.0968652699817,4.67348773080399,7.88450835803408));
#71051=CARTESIAN_POINT('Ctrl Pts',(14.0964383665758,4.50763876447763,7.97977606599027));
#71052=CARTESIAN_POINT('Ctrl Pts',(14.0963267565808,4.46427906756238,8.0046829377923));
#71053=CARTESIAN_POINT('Ctrl Pts',(14.0961289474093,4.42087129224772,8.02950504143281));
#71054=CARTESIAN_POINT('Ctrl Pts',(14.0958463988297,4.37741303746927,8.05424354177964));
#71055=CARTESIAN_POINT('Ctrl Pts',(14.0949720775559,4.24293536027659,8.13079461546704));
#71056=CARTESIAN_POINT('Ctrl Pts',(14.0932865822815,4.10814556901548,8.20644784591187));
#71057=CARTESIAN_POINT('Ctrl Pts',(14.0908378720275,3.97297486435819,8.28124962289842));
#71058=CARTESIAN_POINT('Ctrl Pts',(14.0890335492626,3.87337484872643,8.33636702556368));
#71059=CARTESIAN_POINT('Ctrl Pts',(14.0868149528524,3.77356809910453,8.3910219733713));
#71060=CARTESIAN_POINT('Ctrl Pts',(14.0841559268849,3.6735063041529,8.44524657114381));
#71061=CARTESIAN_POINT('Ctrl Pts',(14.0806813229798,3.54275349928009,8.51610296798621));
#71062=CARTESIAN_POINT('Ctrl Pts',(14.0764615201051,3.41177376280762,8.58611052772096));
#71063=CARTESIAN_POINT('Ctrl Pts',(14.0714486898467,3.28044252824023,8.65536429918285));
#71064=CARTESIAN_POINT('Ctrl Pts',(14.0666278773626,3.1541419709661,8.72196528681374));
#71065=CARTESIAN_POINT('Ctrl Pts',(14.0610735151127,3.02751620452341,8.78786912483827));
#71066=CARTESIAN_POINT('Ctrl Pts',(14.0547625067568,2.90049109865881,8.85313731723337));
#71067=CARTESIAN_POINT('Ctrl Pts',(14.0492174860498,2.78888344381294,8.91048369643663));
#71068=CARTESIAN_POINT('Ctrl Pts',(14.0430885450048,2.67696791838073,8.96733907859141));
#71069=CARTESIAN_POINT('Ctrl Pts',(14.0363741539029,2.56472008839153,9.02372962028756));
#71070=CARTESIAN_POINT('',(14.0357899498033,-2.56414768532805,9.02407043229152));
#71071=CARTESIAN_POINT('Origin',(14.0335933651569,0.,-5.74478136444738E-16));
#71072=CARTESIAN_POINT('',(14.0346021788821,-6.53571152371428,6.73113542385556));
#71073=CARTESIAN_POINT('Ctrl Pts',(14.0363741539029,-2.56472008839153,9.02372962028756));
#71074=CARTESIAN_POINT('Ctrl Pts',(14.043958154477,-2.69150561431106,8.96003569866323));
#71075=CARTESIAN_POINT('Ctrl Pts',(14.050794016563,-2.81788693531343,8.89574019624087));
#71076=CARTESIAN_POINT('Ctrl Pts',(14.0568875375885,-2.94391063651312,8.83079680974982));
#71077=CARTESIAN_POINT('Ctrl Pts',(14.0631313247643,-3.07304208056859,8.76425192018057));
#71078=CARTESIAN_POINT('Ctrl Pts',(14.0685958234893,-3.20179814750712,8.69702680529725));
#71079=CARTESIAN_POINT('Ctrl Pts',(14.0733090155997,-3.33027166381696,8.62904584746018));
#71080=CARTESIAN_POINT('Ctrl Pts',(14.0737328173231,-3.34182377040356,8.6229331224928));
#71081=CARTESIAN_POINT('Ctrl Pts',(14.0741505579373,-3.35337361964161,8.61681426950542));
#71082=CARTESIAN_POINT('Ctrl Pts',(14.0745622655563,-3.36492129486038,8.61068922364988));
#71083=CARTESIAN_POINT('Ctrl Pts',(14.0794394387138,-3.50171743128173,8.53813067029886));
#71084=CARTESIAN_POINT('Ctrl Pts',(14.0834615310167,-3.63801904201261,8.46480359133492));
#71085=CARTESIAN_POINT('Ctrl Pts',(14.0866814188314,-3.77393577056981,8.39063029664073));
#71086=CARTESIAN_POINT('Ctrl Pts',(14.0882552127476,-3.84036818462527,8.35437640002852));
#71087=CARTESIAN_POINT('Ctrl Pts',(14.0896378032368,-3.90670926989839,8.31791993646802));
#71088=CARTESIAN_POINT('Ctrl Pts',(14.0908376694239,-3.97297492845536,8.28124971544124));
#71089=CARTESIAN_POINT('Ctrl Pts',(14.0919557958864,-4.0347263030478,8.24707761779182));
#71090=CARTESIAN_POINT('Ctrl Pts',(14.0929152942353,-4.09641222151593,8.21271986900141));
#71091=CARTESIAN_POINT('Ctrl Pts',(14.0937114070427,-4.15803990964958,8.17817121287961));
#71092=CARTESIAN_POINT('Ctrl Pts',(14.0958985068726,-4.32734494405542,8.08325833215152));
#71093=CARTESIAN_POINT('Ctrl Pts',(14.0968439958899,-4.49592110847136,7.98706849202655));
#71094=CARTESIAN_POINT('Ctrl Pts',(14.0964643580789,-4.66390152282726,7.8895276502587));
#71095=CARTESIAN_POINT('Ctrl Pts',(14.0963723250581,-4.70462387583996,7.86588148527657));
#71096=CARTESIAN_POINT('Ctrl Pts',(14.0962026412765,-4.74531125567541,7.84215584474483));
#71097=CARTESIAN_POINT('Ctrl Pts',(14.0959545618739,-4.78596555791072,7.81834956722898));
#71098=CARTESIAN_POINT('Ctrl Pts',(14.0950534684957,-4.93363328914806,7.7318785470249));
#71099=CARTESIAN_POINT('Ctrl Pts',(14.0931172756096,-5.08065748200534,7.64446522212734));
#71100=CARTESIAN_POINT('Ctrl Pts',(14.0901216005509,-5.22713884336655,7.55606608076033));
#71101=CARTESIAN_POINT('Ctrl Pts',(14.0884090550304,-5.31087823242858,7.50553070873148));
#71102=CARTESIAN_POINT('Ctrl Pts',(14.0863508376835,-5.3944397165887,7.4546733264047));
#71103=CARTESIAN_POINT('Ctrl Pts',(14.0839473935998,-5.47783644876665,7.40348815992946));
#71104=CARTESIAN_POINT('Ctrl Pts',(14.0801455293263,-5.60975674545588,7.32252141014012));
#71105=CARTESIAN_POINT('Ctrl Pts',(14.0754874908681,-5.74104585820757,7.2408678413595));
#71106=CARTESIAN_POINT('Ctrl Pts',(14.0699826640698,-5.87179177769875,7.15849937346112));
#71107=CARTESIAN_POINT('Ctrl Pts',(14.0646793238266,-5.9977521615382,7.07914573953416));
#71108=CARTESIAN_POINT('Ctrl Pts',(14.0585899970416,-6.12320849014614,6.99912844980959));
#71109=CARTESIAN_POINT('Ctrl Pts',(14.0517394686097,-6.24819881250178,6.91844353123771));
#71110=CARTESIAN_POINT('Ctrl Pts',(14.0489440163948,-6.2992028302115,6.88551894205202));
#71111=CARTESIAN_POINT('Ctrl Pts',(14.046022010621,-6.35012876048327,6.85248344327568));
#71112=CARTESIAN_POINT('Ctrl Pts',(14.0429759898737,-6.4009770982182,6.81933789599595));
#71113=CARTESIAN_POINT('Ctrl Pts',(14.0402820510809,-6.44594800319277,6.79002356000296));
#71114=CARTESIAN_POINT('Ctrl Pts',(14.0374911009489,-6.49085821058945,6.76062314763658));
#71115=CARTESIAN_POINT('Ctrl Pts',(14.0346021788821,-6.53571152371428,6.73113542385556));
#71116=CARTESIAN_POINT('',(14.0346124314935,-9.09718908205277,2.29451127187482));
#71117=CARTESIAN_POINT('Origin',(14.0335933651569,0.,-5.74478136444738E-16));
#71118=CARTESIAN_POINT('Ctrl Pts',(14.0346846831548,-9.09718960292737,2.2945529963785));
#71119=CARTESIAN_POINT('Ctrl Pts',(14.0375755696933,-9.10029985513173,2.24096964017332));
#71120=CARTESIAN_POINT('Ctrl Pts',(14.0403683507454,-9.10330641202519,2.18737754787371));
#71121=CARTESIAN_POINT('Ctrl Pts',(14.043064127072,-9.10620834784861,2.13377218640334));
#71122=CARTESIAN_POINT('Ctrl Pts',(14.0505699144896,-9.11428814036506,1.98452002343198));
#71123=CARTESIAN_POINT('Ctrl Pts',(14.0573226099962,-9.12155698997562,1.83516862172181));
#71124=CARTESIAN_POINT('Ctrl Pts',(14.063291784655,-9.1279976635329,1.68568903225001));
#71125=CARTESIAN_POINT('Ctrl Pts',(14.0671820861081,-9.13219525585202,1.58826841761204));
#71126=CARTESIAN_POINT('Ctrl Pts',(14.0707399396716,-9.1360410552266,1.49079227060918));
#71127=CARTESIAN_POINT('Ctrl Pts',(14.0739605337436,-9.13952991576929,1.39324130828922));
#71128=CARTESIAN_POINT('Ctrl Pts',(14.0793070342071,-9.14532176475466,1.23129719065468));
#71129=CARTESIAN_POINT('Ctrl Pts',(14.0837153543482,-9.15012154561397,1.06937897158109));
#71130=CARTESIAN_POINT('Ctrl Pts',(14.0871728595392,-9.1539180726121,0.907429557794384));
#71131=CARTESIAN_POINT('Ctrl Pts',(14.0901574685142,-9.15719533408431,0.767630585072405));
#71132=CARTESIAN_POINT('Ctrl Pts',(14.0924341327935,-9.15972498534995,0.627807045687021));
#71133=CARTESIAN_POINT('Ctrl Pts',(14.0940107917454,-9.16149748328792,0.487895780218749));
#71134=CARTESIAN_POINT('Ctrl Pts',(14.0958453211638,-9.16355988213915,0.325101326699524));
#71135=CARTESIAN_POINT('Ctrl Pts',(14.0967276209543,-9.16459504304142,0.162420881184377));
#71136=CARTESIAN_POINT('Ctrl Pts',(14.0966872156073,-9.1646003104954,-0.000235982960761354));
#71137=CARTESIAN_POINT('Ctrl Pts',(12.6361849146756,-0.403980496774264,
-10.7652843795024));
#71138=CARTESIAN_POINT('Ctrl Pts',(13.1323548632684,-1.83314667576049,-9.94015490134798));
#71139=CARTESIAN_POINT('Ctrl Pts',(13.5259820957649,-3.8118564888613,-8.79774625810608));
#71140=CARTESIAN_POINT('Ctrl Pts',(13.3920458446166,-6.48443612385918,-7.25473168640934));
#71141=CARTESIAN_POINT('Ctrl Pts',(12.9669648804042,-8.16824205056825,-6.28258588136077));
#71142=CARTESIAN_POINT('Ctrl Pts',(12.6361849146757,-9.12101950322573,-5.73249956259117));
#71143=CARTESIAN_POINT('Ctrl Pts',(12.8699890291072,-0.269320331182842,
-10.6726380968212));
#71144=CARTESIAN_POINT('Ctrl Pts',(13.3767756515671,-1.71258108335182,-9.84301179383112));
#71145=CARTESIAN_POINT('Ctrl Pts',(13.7845689781422,-3.72407315433307,-8.68667090248932));
#71146=CARTESIAN_POINT('Ctrl Pts',(13.6453803397493,-6.44473655178331,-7.11403939432886));
#71147=CARTESIAN_POINT('Ctrl Pts',(13.2078467774138,-8.14804366490556,-6.12628217974948));
#71148=CARTESIAN_POINT('Ctrl Pts',(12.8699890291072,-9.10811555165335,-5.56955729697059));
#71149=CARTESIAN_POINT('Ctrl Pts',(13.1037931435388,-0.134660165591419,
-10.57999181414));
#71150=CARTESIAN_POINT('Ctrl Pts',(13.6211964398659,-1.59201549094316,-9.74586868631425));
#71151=CARTESIAN_POINT('Ctrl Pts',(14.0431558605194,-3.63628981980485,-8.57559554687257));
#71152=CARTESIAN_POINT('Ctrl Pts',(13.898714834882,-6.40503697970743,-6.97334710224838));
#71153=CARTESIAN_POINT('Ctrl Pts',(13.4487286744235,-8.12784527924288,-5.96997847813818));
#71154=CARTESIAN_POINT('Ctrl Pts',(13.1037931435388,-9.09521160008097,-5.40661503135001));
#71155=CARTESIAN_POINT('Ctrl Pts',(13.3375972579703,2.97082320207775E-15,
-10.4873455314589));
#71156=CARTESIAN_POINT('Ctrl Pts',(13.8656172281646,-1.4714498985345,-9.64872557879739));
#71157=CARTESIAN_POINT('Ctrl Pts',(14.3017427428967,-3.54850648527662,-8.46452019125581));
#71158=CARTESIAN_POINT('Ctrl Pts',(14.1520493300147,-6.36533740763157,-6.83265481016789));
#71159=CARTESIAN_POINT('Ctrl Pts',(13.6896105714332,-8.1076468935802,-5.81367477652689));
#71160=CARTESIAN_POINT('Ctrl Pts',(13.3375972579703,-9.08230764850859,-5.24367276572944));
#71161=CARTESIAN_POINT('',(13.3375972579703,-9.0823076485086,-5.24367276572943));
#71162=CARTESIAN_POINT('Ctrl Pts',(14.0346021788807,-6.53571152372215,-6.73113542385098));
#71163=CARTESIAN_POINT('Ctrl Pts',(13.8952900661411,-7.33167501862017,-6.26749768919284));
#71164=CARTESIAN_POINT('Ctrl Pts',(13.6704419928349,-8.16072119666195,-5.78263581314881));
#71165=CARTESIAN_POINT('Ctrl Pts',(13.3375972579703,-9.08230764850859,-5.24367276572944));
#71166=CARTESIAN_POINT('',(12.6462384144175,-9.0919872981105,-5.74926131402961));
#71167=CARTESIAN_POINT('Ctrl Pts',(12.6462384144175,-9.0919872981105,-5.74926131402961));
#71168=CARTESIAN_POINT('Ctrl Pts',(12.7615608863228,-9.0902706516109,-5.66510306978528));
#71169=CARTESIAN_POINT('Ctrl Pts',(12.8768443884274,-9.08860556242311,-5.58088496917862));
#71170=CARTESIAN_POINT('Ctrl Pts',(13.1072956815908,-9.08537904841867,-5.41235664115676));
#71171=CARTESIAN_POINT('Ctrl Pts',(13.2224686011676,-9.08381752761855,-5.32804270515258));
#71172=CARTESIAN_POINT('Ctrl Pts',(13.3375972579703,-9.08230764850859,-5.24367276572944));
#71173=CARTESIAN_POINT('',(12.6462384144167,-0.433012701892221,-10.7485226280624));
#71174=CARTESIAN_POINT('Ctrl Pts',(12.6462397169616,-9.09198644037733,-5.7492618092421));
#71175=CARTESIAN_POINT('Ctrl Pts',(12.9712786667833,-8.15112288573813,-6.29246963578375));
#71176=CARTESIAN_POINT('Ctrl Pts',(13.3924350002713,-6.47667086636881,-7.25921495991174));
#71177=CARTESIAN_POINT('Ctrl Pts',(13.5255929401102,-3.81962174635228,-8.79326298460333));
#71178=CARTESIAN_POINT('Ctrl Pts',(13.1355491140167,-1.84924327825312,-9.93086152356582));
#71179=CARTESIAN_POINT('Ctrl Pts',(12.6462405439417,-0.433014589690331,
-10.7485215381416));
#71180=CARTESIAN_POINT('',(13.3375972579703,-1.68649378841241E-15,-10.4873455314589));
#71181=CARTESIAN_POINT('Ctrl Pts',(13.3375972579703,2.97082320207775E-15,
-10.4873455314589));
#71182=CARTESIAN_POINT('Ctrl Pts',(13.2224673861593,-0.0723123344410041,
-10.530838553834));
#71183=CARTESIAN_POINT('Ctrl Pts',(13.1072932506126,-0.144550346101911,
-10.5743482978785));
#71184=CARTESIAN_POINT('Ctrl Pts',(12.8768419556923,-0.288886899219771,
-10.6614067056461));
#71185=CARTESIAN_POINT('Ctrl Pts',(12.7615596695621,-0.360988607620142,
-10.7049573061223));
#71186=CARTESIAN_POINT('Ctrl Pts',(12.6462384144189,-0.433012701893692,
-10.7485226280615));
#71187=CARTESIAN_POINT('Ctrl Pts',(13.3375972579703,2.97082320207775E-15,
-10.4873455314589));
#71188=CARTESIAN_POINT('Ctrl Pts',(13.6704419928349,-0.927548916689568,
-9.9587097760858));
#71189=CARTESIAN_POINT('Ctrl Pts',(13.8974523690185,-1.765606325871,-9.48097436223191));
#71190=CARTESIAN_POINT('Ctrl Pts',(14.0363741539015,-2.56472008838367,-9.02372962029205));
#71191=CARTESIAN_POINT('Ctrl Pts',(12.6361849146756,-9.525,-5.03278481691122));
#71192=CARTESIAN_POINT('Ctrl Pts',(13.1323548632684,-9.525,-3.38252586060241));
#71193=CARTESIAN_POINT('Ctrl Pts',(13.5261795528199,-9.525,-1.0975656251991));
#71194=CARTESIAN_POINT('Ctrl Pts',(13.3921464946308,-9.525,1.98832724851365));
#71195=CARTESIAN_POINT('Ctrl Pts',(12.9669648804042,-9.525,3.93261217937201));
#71196=CARTESIAN_POINT('Ctrl Pts',(12.6361849146757,-9.525,5.03278481691122));
#71197=CARTESIAN_POINT('Ctrl Pts',(12.8699890291072,-9.3774358828362,-5.10308079985063));
#71198=CARTESIAN_POINT('Ctrl Pts',(13.3767756515671,-9.3805888048835,-3.4383671726922));
#71199=CARTESIAN_POINT('Ctrl Pts',(13.7847648925596,-9.38491352314618,-1.11803995403544));
#71200=CARTESIAN_POINT('Ctrl Pts',(13.6454811073302,-9.38330701946683,2.02429453530628));
#71201=CARTESIAN_POINT('Ctrl Pts',(13.2078467774138,-9.37953783086773,3.99327171507834));
#71202=CARTESIAN_POINT('Ctrl Pts',(12.8699890291072,-9.3774358828362,5.10308079985062));
#71203=CARTESIAN_POINT('Ctrl Pts',(13.1037931435388,-9.2298717656724,-5.17337678279003));
#71204=CARTESIAN_POINT('Ctrl Pts',(13.6211964398659,-9.236177609767,-3.49420848478199));
#71205=CARTESIAN_POINT('Ctrl Pts',(14.0433502322992,-9.24482704629237,-1.13851428287178));
#71206=CARTESIAN_POINT('Ctrl Pts',(13.8988157200297,-9.24161403893367,2.06026182209891));
#71207=CARTESIAN_POINT('Ctrl Pts',(13.4487286744235,-9.23407566173547,4.05393125078467));
#71208=CARTESIAN_POINT('Ctrl Pts',(13.1037931435388,-9.2298717656724,5.17337678279003));
#71209=CARTESIAN_POINT('Ctrl Pts',(13.3375972579703,-9.0823076485086,-5.24367276572943));
#71210=CARTESIAN_POINT('Ctrl Pts',(13.8656172281646,-9.09176641465051,-3.55004979687178));
#71211=CARTESIAN_POINT('Ctrl Pts',(14.3019355720389,-9.10474056943856,-1.15898861170811));
#71212=CARTESIAN_POINT('Ctrl Pts',(14.1521503327292,-9.0999210584005,2.09622910889154));
#71213=CARTESIAN_POINT('Ctrl Pts',(13.6896105714332,-9.0886134926032,4.114590786491));
#71214=CARTESIAN_POINT('Ctrl Pts',(13.3375972579703,-9.08230764850859,5.24367276572943));
#71215=CARTESIAN_POINT('',(13.3375972579703,-9.08230764850859,5.24367276572943));
#71216=CARTESIAN_POINT('Ctrl Pts',(14.0346846831534,-9.09718960292733,2.29455299638773));
#71217=CARTESIAN_POINT('Ctrl Pts',(13.8953352172327,-9.09364959832235,3.21567361322219));
#71218=CARTESIAN_POINT('Ctrl Pts',(13.6704419928349,-9.08827011335153,4.17607396293699));
#71219=CARTESIAN_POINT('Ctrl Pts',(13.3375972579703,-9.08230764850859,5.24367276572943));
#71220=CARTESIAN_POINT('',(12.6462384144175,-9.525,4.99926131403433));
#71221=CARTESIAN_POINT('Ctrl Pts',(12.6462384144175,-9.525,4.99926131403433));
#71222=CARTESIAN_POINT('Ctrl Pts',(12.761560886318,-9.45125849929978,5.03985377667684));
#71223=CARTESIAN_POINT('Ctrl Pts',(12.8768443884248,-9.37749094012068,5.08052081744472));
#71224=CARTESIAN_POINT('Ctrl Pts',(13.1072956815865,-9.22992786979522,5.16199073836157));
#71225=CARTESIAN_POINT('Ctrl Pts',(13.2224686011656,-9.1561290989211,5.20279538968299));
#71226=CARTESIAN_POINT('Ctrl Pts',(13.3375972579703,-9.08230764850859,5.24367276572943));
#71227=CARTESIAN_POINT('',(12.6462384144167,-9.525,-4.99926131403118));
#71228=CARTESIAN_POINT('Ctrl Pts',(12.6462397325099,-9.525,4.99926032466067));
#71229=CARTESIAN_POINT('Ctrl Pts',(12.9712796891567,-9.525,3.91284474029011));
#71230=CARTESIAN_POINT('Ctrl Pts',(13.3925359315611,-9.525,1.97936109744437));
#71231=CARTESIAN_POINT('Ctrl Pts',(13.5257901158896,-9.525,-1.08859947412911));
#71232=CARTESIAN_POINT('Ctrl Pts',(13.1355507160135,-9.525,-3.36393794605574));
#71233=CARTESIAN_POINT('Ctrl Pts',(12.646240560211,-9.525,-4.99925912241684));
#71234=CARTESIAN_POINT('Ctrl Pts',(13.3375972579703,-9.0823076485086,-5.24367276572943));
#71235=CARTESIAN_POINT('Ctrl Pts',(13.2224673861572,-9.15612987799469,-5.20279495828338));
#71236=CARTESIAN_POINT('Ctrl Pts',(13.1072932506082,-9.22992942748129,-5.16198987708763));
#71237=CARTESIAN_POINT('Ctrl Pts',(12.8768419556921,-9.37749249677728,-5.08051995927811));
#71238=CARTESIAN_POINT('Ctrl Pts',(12.7615596695613,-9.45125927734028,-5.03985334838505));
#71239=CARTESIAN_POINT('Ctrl Pts',(12.6462384144189,-9.525,-4.99926131402949));
#71240=CARTESIAN_POINT('Ctrl Pts',(13.3375972579703,-9.0823076485086,-5.24367276572943));
#71241=CARTESIAN_POINT('Ctrl Pts',(13.6704419928349,-9.08827011335153,-4.176073962937));
#71242=CARTESIAN_POINT('Ctrl Pts',(13.8974983424166,-9.09356729120583,-3.21138559340686));
#71243=CARTESIAN_POINT('Ctrl Pts',(14.0364597916673,-9.09713821521857,-2.29067954585915));
#71244=CARTESIAN_POINT('Origin',(13.55,0.,0.));
#71245=CARTESIAN_POINT('Origin',(13.55,0.,0.));
#71246=CARTESIAN_POINT('Ctrl Pts',(13.3375972579703,-9.0823076485086,5.24367276572943));
#71247=CARTESIAN_POINT('Ctrl Pts',(13.6704419928349,-8.16072119666196,5.7826358131488));
#71248=CARTESIAN_POINT('Ctrl Pts',(13.8952900661411,-7.33167501862017,6.26749768919284));
#71249=CARTESIAN_POINT('Ctrl Pts',(14.0346021788807,-6.53571152372215,6.73113542385098));
#71250=CARTESIAN_POINT('Origin',(13.55,0.,0.));
#71251=CARTESIAN_POINT('',(13.3375972579703,6.4216470683267E-16,10.4873455314589));
#71252=CARTESIAN_POINT('Ctrl Pts',(13.3375972579703,6.4216470683267E-16,
10.4873455314589));
#71253=CARTESIAN_POINT('Ctrl Pts',(13.6704419928349,0.927548916689572,9.9587097760858));
#71254=CARTESIAN_POINT('Ctrl Pts',(13.8974523690185,1.76560632587101,9.4809743622319));
#71255=CARTESIAN_POINT('Ctrl Pts',(14.0363741539015,2.56472008838367,9.02372962029205));
#71256=CARTESIAN_POINT('Ctrl Pts',(14.0363741539015,-2.56472008838366,9.02372962029206));
#71257=CARTESIAN_POINT('Ctrl Pts',(13.8974523690185,-1.765606325871,9.48097436223191));
#71258=CARTESIAN_POINT('Ctrl Pts',(13.6704419928349,-0.927548916689566,
9.9587097760858));
#71259=CARTESIAN_POINT('Ctrl Pts',(13.3375972579703,2.97082320207775E-15,
10.4873455314589));
#71260=CARTESIAN_POINT('Origin',(13.55,0.,0.));
#71261=CARTESIAN_POINT('',(13.3375972579703,9.08230764850859,5.24367276572943));
#71262=CARTESIAN_POINT('Ctrl Pts',(13.3375972579703,9.08230764850859,5.24367276572943));
#71263=CARTESIAN_POINT('Ctrl Pts',(13.6704419928349,9.08827011335153,4.17607396293699));
#71264=CARTESIAN_POINT('Ctrl Pts',(13.8974983424166,9.09356729120583,3.21138559340686));
#71265=CARTESIAN_POINT('Ctrl Pts',(14.0364597916673,9.09713821521856,2.29067954585916));
#71266=CARTESIAN_POINT('Ctrl Pts',(14.0346021788807,6.53571152372216,6.73113542385098));
#71267=CARTESIAN_POINT('Ctrl Pts',(13.8952900661411,7.33167501862018,6.26749768919284));
#71268=CARTESIAN_POINT('Ctrl Pts',(13.6704419928349,8.16072119666196,5.7826358131488));
#71269=CARTESIAN_POINT('Ctrl Pts',(13.3375972579703,9.0823076485086,5.24367276572943));
#71270=CARTESIAN_POINT('Origin',(13.55,0.,0.));
#71271=CARTESIAN_POINT('',(13.3375972579703,9.08230764850859,-5.24367276572944));
#71272=CARTESIAN_POINT('Ctrl Pts',(13.3375972579703,9.08230764850859,-5.24367276572944));
#71273=CARTESIAN_POINT('Ctrl Pts',(13.6704419928349,8.16072119666195,-5.78263581314881));
#71274=CARTESIAN_POINT('Ctrl Pts',(13.8952900661411,7.33167501862017,-6.26749768919285));
#71275=CARTESIAN_POINT('Ctrl Pts',(14.0346021788807,6.53571152372214,-6.73113542385099));
#71276=CARTESIAN_POINT('Ctrl Pts',(14.0346846831534,9.09718960292733,-2.29455299638774));
#71277=CARTESIAN_POINT('Ctrl Pts',(13.8953352172327,9.09364959832235,-3.2156736132222));
#71278=CARTESIAN_POINT('Ctrl Pts',(13.6704419928349,9.08827011335152,-4.176073962937));
#71279=CARTESIAN_POINT('Ctrl Pts',(13.3375972579703,9.08230764850859,-5.24367276572944));
#71280=CARTESIAN_POINT('Origin',(13.55,0.,0.));
#71281=CARTESIAN_POINT('Ctrl Pts',(14.0363741539015,2.56472008838366,-9.02372962029206));
#71282=CARTESIAN_POINT('Ctrl Pts',(13.8974523690185,1.76560632587099,-9.48097436223191));
#71283=CARTESIAN_POINT('Ctrl Pts',(13.6704419928349,0.927548916689562,-9.9587097760858));
#71284=CARTESIAN_POINT('Ctrl Pts',(13.3375972579703,-6.34381077890256E-15,
-10.4873455314589));
#71285=CARTESIAN_POINT('Ctrl Pts',(12.6361849146756,-9.12101950322574,5.73249956259117));
#71286=CARTESIAN_POINT('Ctrl Pts',(12.9669648804042,-8.16824205056825,6.28258588136077));
#71287=CARTESIAN_POINT('Ctrl Pts',(13.3920458446166,-6.48443612385918,7.25473168640934));
#71288=CARTESIAN_POINT('Ctrl Pts',(13.5259820957649,-3.8118564888613,8.79774625810608));
#71289=CARTESIAN_POINT('Ctrl Pts',(13.1323548632684,-1.83314667576049,9.94015490134798));
#71290=CARTESIAN_POINT('Ctrl Pts',(12.6361849146756,-0.403980496774266,
10.7652843795024));
#71291=CARTESIAN_POINT('Ctrl Pts',(12.8699890291072,-9.10811555165336,5.56955729697059));
#71292=CARTESIAN_POINT('Ctrl Pts',(13.2078467774138,-8.14804366490556,6.12628217974948));
#71293=CARTESIAN_POINT('Ctrl Pts',(13.6453803397493,-6.4447365517833,7.11403939432885));
#71294=CARTESIAN_POINT('Ctrl Pts',(13.7845689781422,-3.72407315433307,8.68667090248933));
#71295=CARTESIAN_POINT('Ctrl Pts',(13.3767756515671,-1.71258108335183,9.84301179383112));
#71296=CARTESIAN_POINT('Ctrl Pts',(12.8699890291072,-0.269320331182843,
10.6726380968212));
#71297=CARTESIAN_POINT('Ctrl Pts',(13.1037931435388,-9.09521160008098,5.40661503135001));
#71298=CARTESIAN_POINT('Ctrl Pts',(13.4487286744235,-8.12784527924288,5.96997847813818));
#71299=CARTESIAN_POINT('Ctrl Pts',(13.898714834882,-6.40503697970743,6.97334710224837));
#71300=CARTESIAN_POINT('Ctrl Pts',(14.0431558605194,-3.63628981980485,8.57559554687257));
#71301=CARTESIAN_POINT('Ctrl Pts',(13.6211964398659,-1.59201549094317,9.74586868631425));
#71302=CARTESIAN_POINT('Ctrl Pts',(13.1037931435388,-0.13466016559142,10.57999181414));
#71303=CARTESIAN_POINT('Ctrl Pts',(13.3375972579703,-9.0823076485086,5.24367276572943));
#71304=CARTESIAN_POINT('Ctrl Pts',(13.6896105714332,-8.1076468935802,5.81367477652688));
#71305=CARTESIAN_POINT('Ctrl Pts',(14.1520493300147,-6.36533740763156,6.83265481016789));
#71306=CARTESIAN_POINT('Ctrl Pts',(14.3017427428967,-3.54850648527663,8.46452019125581));
#71307=CARTESIAN_POINT('Ctrl Pts',(13.8656172281646,-1.4714498985345,9.64872557879739));
#71308=CARTESIAN_POINT('Ctrl Pts',(13.3375972579703,2.97082320207775E-15,
10.4873455314589));
#71309=CARTESIAN_POINT('',(12.6462384144175,-0.433012701889492,10.7485226280639));
#71310=CARTESIAN_POINT('Ctrl Pts',(12.6462384144175,-0.43301270188949,10.7485226280639));
#71311=CARTESIAN_POINT('Ctrl Pts',(12.7615608863277,-0.360987847682757,
10.704956846462));
#71312=CARTESIAN_POINT('Ctrl Pts',(12.8768443884298,-0.288885377694372,
10.6614057866234));
#71313=CARTESIAN_POINT('Ctrl Pts',(13.1072956816033,-0.144548821365988,
10.5743473795151));
#71314=CARTESIAN_POINT('Ctrl Pts',(13.2224686011745,-0.0723115712969127,
10.5308380948337));
#71315=CARTESIAN_POINT('Ctrl Pts',(13.3375972579703,2.97082320207775E-15,
10.4873455314589));
#71316=CARTESIAN_POINT('',(12.6462384144167,-9.09198729810778,5.74926131403119));
#71317=CARTESIAN_POINT('Ctrl Pts',(12.6462405439409,-0.433014589688018,
10.748521538143));
#71318=CARTESIAN_POINT('Ctrl Pts',(13.1355491140165,-1.84924327825184,9.93086152356656));
#71319=CARTESIAN_POINT('Ctrl Pts',(13.5255929401103,-3.81962174635166,8.79326298460369));
#71320=CARTESIAN_POINT('Ctrl Pts',(13.3924350002713,-6.47667086636819,7.25921495991209));
#71321=CARTESIAN_POINT('Ctrl Pts',(12.9712786667837,-8.15112288573676,6.29246963578453));
#71322=CARTESIAN_POINT('Ctrl Pts',(12.6462397169624,-9.09198644037501,5.74926180924343));
#71323=CARTESIAN_POINT('Ctrl Pts',(13.3375972579703,-9.0823076485086,5.24367276572943));
#71324=CARTESIAN_POINT('Ctrl Pts',(13.2224673861609,-9.08381754355231,5.32804359554874));
#71325=CARTESIAN_POINT('Ctrl Pts',(13.1072932506156,-9.08537908137654,5.41235842078712));
#71326=CARTESIAN_POINT('Ctrl Pts',(12.8768419556905,-9.08860559755739,5.58088674636916));
#71327=CARTESIAN_POINT('Ctrl Pts',(12.7615596695584,-9.0902706697197,5.66510395773964));
#71328=CARTESIAN_POINT('Ctrl Pts',(12.6462384144189,-9.09198729810631,5.74926131403204));
#71329=CARTESIAN_POINT('Origin',(14.3,0.,0.));
#71330=CARTESIAN_POINT('',(14.3,-7.1,8.69499227394621E-16));
#71331=CARTESIAN_POINT('Origin',(14.3,0.,0.));
#71332=CARTESIAN_POINT('Origin',(3.,-9.025,5.21058617943637));
#71333=CARTESIAN_POINT('',(3.5,-9.09198729810778,5.74926131403119));
#71334=CARTESIAN_POINT('',(3.5,-9.525,4.99926131403119));
#71335=CARTESIAN_POINT('',(3.5,-9.09198729810778,5.74926131403119));
#71336=CARTESIAN_POINT('',(3.,-9.025,5.21058617943637));
#71337=CARTESIAN_POINT('',(3.,-9.025,5.21058617943637));
#71338=CARTESIAN_POINT('',(3.5,-9.525,4.99926131403119));
#71339=CARTESIAN_POINT('Origin',(3.,2.22044604925031E-15,10.4211723588727));
#71340=CARTESIAN_POINT('',(3.5,0.433012701892219,10.7485226280624));
#71341=CARTESIAN_POINT('',(3.5,-0.433012701892217,10.7485226280624));
#71342=CARTESIAN_POINT('',(3.5,0.433012701892221,10.7485226280624));
#71343=CARTESIAN_POINT('',(3.,3.60822483003176E-15,10.4211723588727));
#71344=CARTESIAN_POINT('',(3.,2.22044604925031E-15,10.4211723588727));
#71345=CARTESIAN_POINT('',(3.5,-0.433012701892217,10.7485226280624));
#71346=CARTESIAN_POINT('Origin',(3.,-9.025,-5.21058617943637));
#71347=CARTESIAN_POINT('',(3.5,-9.525,-4.99926131403118));
#71348=CARTESIAN_POINT('',(3.5,-9.09198729810778,-5.74926131403119));
#71349=CARTESIAN_POINT('',(3.5,-9.525,-4.99926131403118));
#71350=CARTESIAN_POINT('',(3.,-9.025,-5.21058617943637));
#71351=CARTESIAN_POINT('',(3.,-9.025,-5.21058617943637));
#71352=CARTESIAN_POINT('',(3.5,-9.09198729810778,-5.74926131403119));
#71353=CARTESIAN_POINT('Origin',(3.25,-9.275,2.74963065701559));
#71354=CARTESIAN_POINT('',(3.5,-9.525,2.74963065701559));
#71355=CARTESIAN_POINT('',(3.,-9.025,2.74963065701559));
#71356=CARTESIAN_POINT('Origin',(12.6462384144175,-9.525,4.99926131403433));
#71357=CARTESIAN_POINT('',(12.6462384144167,-9.525,4.99926131403119));
#71358=CARTESIAN_POINT('Origin',(3.,9.025,5.21058617943637));
#71359=CARTESIAN_POINT('',(3.5,9.525,4.99926131403119));
#71360=CARTESIAN_POINT('',(3.5,9.09198729810778,5.74926131403119));
#71361=CARTESIAN_POINT('',(3.5,9.525,4.99926131403119));
#71362=CARTESIAN_POINT('',(3.,9.025,5.21058617943637));
#71363=CARTESIAN_POINT('',(3.,9.025,5.21058617943637));
#71364=CARTESIAN_POINT('',(3.5,9.09198729810778,5.74926131403119));
#71365=CARTESIAN_POINT('Origin',(13.3375972579703,6.4216470683267E-16,10.4873455314589));
#71366=CARTESIAN_POINT('',(12.6462384144167,0.433012701892221,10.7485226280624));
#71367=CARTESIAN_POINT('Ctrl Pts',(13.3375972579703,7.6281401925679E-15,
10.4873455314589));
#71368=CARTESIAN_POINT('Ctrl Pts',(13.2224673861555,0.0723123344434218,
10.5308385538355));
#71369=CARTESIAN_POINT('Ctrl Pts',(13.1072932506048,0.14455034610674,10.5743482978814));
#71370=CARTESIAN_POINT('Ctrl Pts',(12.8768419556913,0.288886899220415,10.6614067056464));
#71371=CARTESIAN_POINT('Ctrl Pts',(12.7615596695601,0.36098860762136,10.704957306123));
#71372=CARTESIAN_POINT('Ctrl Pts',(12.6462384144189,0.433012701893687,10.7485226280615));
#71373=CARTESIAN_POINT('',(12.6462384144167,-0.433012701892217,10.7485226280624));
#71374=CARTESIAN_POINT('Origin',(3.,0.,-10.4211723588727));
#71375=CARTESIAN_POINT('',(3.5,-0.433012701892219,-10.7485226280624));
#71376=CARTESIAN_POINT('',(3.5,0.433012701892217,-10.7485226280624));
#71377=CARTESIAN_POINT('',(3.5,-0.433012701892221,-10.7485226280624));
#71378=CARTESIAN_POINT('',(3.,-1.38777878078145E-15,-10.4211723588727));
#71379=CARTESIAN_POINT('',(3.,0.,-10.4211723588727));
#71380=CARTESIAN_POINT('',(3.5,0.433012701892217,-10.7485226280624));
#71381=CARTESIAN_POINT('Origin',(3.25,-7.01875,-6.65757029159287));
#71382=CARTESIAN_POINT('',(3.5,-7.14375,-6.87407664253898));
#71383=CARTESIAN_POINT('',(3.,-6.89375,-6.44106394064676));
#71384=CARTESIAN_POINT('Origin',(12.6462384144175,-9.0919872981105,-5.74926131402961));
#71385=CARTESIAN_POINT('',(12.6462384144167,-9.09198729810778,-5.74926131403119));
#71386=CARTESIAN_POINT('Origin',(3.5,9.525,-4.99926131403119));
#71387=CARTESIAN_POINT('',(3.,9.025,-5.21058617943638));
#71388=CARTESIAN_POINT('',(3.5,9.09198729810778,-5.74926131403119));
#71389=CARTESIAN_POINT('',(3.,9.025,-5.21058617943638));
#71390=CARTESIAN_POINT('',(3.5,9.525,-4.99926131403119));
#71391=CARTESIAN_POINT('',(3.5,9.525,-4.99926131403119));
#71392=CARTESIAN_POINT('',(3.5,9.09198729810778,-5.74926131403119));
#71393=CARTESIAN_POINT('Origin',(3.25,9.275,-2.7496306570156));
#71394=CARTESIAN_POINT('',(3.5,9.525,-2.7496306570156));
#71395=CARTESIAN_POINT('',(3.,9.025,-2.7496306570156));
#71396=CARTESIAN_POINT('Origin',(13.3375972579703,9.08230764850859,5.24367276572943));
#71397=CARTESIAN_POINT('',(12.6462384144175,9.0919872981105,5.74926131402961));
#71398=CARTESIAN_POINT('Ctrl Pts',(12.6462384144175,9.09198729811051,5.74926131402961));
#71399=CARTESIAN_POINT('Ctrl Pts',(12.7615608863187,9.09027065161096,5.66510306978824));
#71400=CARTESIAN_POINT('Ctrl Pts',(12.8768443884255,9.08860556242314,5.58088496918004));
#71401=CARTESIAN_POINT('Ctrl Pts',(13.1072956816019,9.08537904841851,5.41235664114861));
#71402=CARTESIAN_POINT('Ctrl Pts',(13.2224686011735,9.08381752761848,5.32804270514828));
#71403=CARTESIAN_POINT('Ctrl Pts',(13.3375972579703,9.0823076485086,5.24367276572943));
#71404=CARTESIAN_POINT('',(12.6462384144167,9.525,4.99926131403119));
#71405=CARTESIAN_POINT('Ctrl Pts',(13.3375972579703,9.08230764850859,5.24367276572942));
#71406=CARTESIAN_POINT('Ctrl Pts',(13.2224673861562,9.15612987799533,5.20279495828302));
#71407=CARTESIAN_POINT('Ctrl Pts',(13.1072932506068,9.22992942748221,5.16198987708712));
#71408=CARTESIAN_POINT('Ctrl Pts',(12.8768419556941,9.37749249677602,5.08051995927881));
#71409=CARTESIAN_POINT('Ctrl Pts',(12.7615596695645,9.45125927733824,5.03985334838617));
#71410=CARTESIAN_POINT('Ctrl Pts',(12.6462384144189,9.525,4.99926131402949));
#71411=CARTESIAN_POINT('',(12.6462384144167,9.09198729810778,5.74926131403119));
#71412=CARTESIAN_POINT('Origin',(12.6462384144175,0.433012701889492,-10.7485226280639));
#71413=CARTESIAN_POINT('',(12.6462384144175,0.433012701889492,-10.7485226280639));
#71414=CARTESIAN_POINT('',(12.6462384144167,0.433012701892217,-10.7485226280624));
#71415=CARTESIAN_POINT('Ctrl Pts',(12.6462384144175,0.433012701889488,-10.7485226280639));
#71416=CARTESIAN_POINT('Ctrl Pts',(12.7615608863249,0.360987847684519,-10.704956846463));
#71417=CARTESIAN_POINT('Ctrl Pts',(12.8768443884286,0.288885377695135,-10.6614057866238));
#71418=CARTESIAN_POINT('Ctrl Pts',(13.1072956815852,0.144548821377305,-10.5743473795219));
#71419=CARTESIAN_POINT('Ctrl Pts',(13.2224686011646,0.0723115713031384,
-10.5308380948375));
#71420=CARTESIAN_POINT('Ctrl Pts',(13.3375972579703,-6.34381077890256E-15,
-10.4873455314589));
#71421=CARTESIAN_POINT('Origin',(13.3375972579703,9.08230764850859,-5.24367276572944));
#71422=CARTESIAN_POINT('',(12.6462384144175,9.525,-4.99926131403433));
#71423=CARTESIAN_POINT('Ctrl Pts',(12.6462384144175,9.525,-4.99926131403433));
#71424=CARTESIAN_POINT('Ctrl Pts',(12.7615608863322,9.45125849929071,-5.03985377668183));
#71425=CARTESIAN_POINT('Ctrl Pts',(12.8768443884316,9.37749094011633,-5.08052081744712));
#71426=CARTESIAN_POINT('Ctrl Pts',(13.1072956815797,9.22992786979956,-5.16199073835919));
#71427=CARTESIAN_POINT('Ctrl Pts',(13.2224686011626,9.15612909892297,-5.20279538968195));
#71428=CARTESIAN_POINT('Ctrl Pts',(13.3375972579703,9.08230764850859,-5.24367276572943));
#71429=CARTESIAN_POINT('',(12.6462384144167,9.09198729810778,-5.74926131403119));
#71430=CARTESIAN_POINT('Ctrl Pts',(13.3375972579703,9.08230764850859,-5.24367276572944));
#71431=CARTESIAN_POINT('Ctrl Pts',(13.2224673861615,9.08381754355229,-5.32804359554833));
#71432=CARTESIAN_POINT('Ctrl Pts',(13.1072932506172,9.08537908137651,-5.41235842078597));
#71433=CARTESIAN_POINT('Ctrl Pts',(12.8768419556896,9.0886055975574,-5.58088674636987));
#71434=CARTESIAN_POINT('Ctrl Pts',(12.7615596695564,9.09027066971973,-5.66510395774111));
#71435=CARTESIAN_POINT('Ctrl Pts',(12.6462384144189,9.09198729810631,-5.74926131403204));
#71436=CARTESIAN_POINT('',(12.6462384144167,9.525,-4.99926131403119));
#71437=CARTESIAN_POINT('Ctrl Pts',(12.6361849146757,9.12101950322573,-5.73249956259117));
#71438=CARTESIAN_POINT('Ctrl Pts',(12.9669648804042,8.16824205056824,-6.28258588136078));
#71439=CARTESIAN_POINT('Ctrl Pts',(13.3920458446166,6.48443612385917,-7.25473168640934));
#71440=CARTESIAN_POINT('Ctrl Pts',(13.5259820957649,3.81185648886129,-8.79774625810609));
#71441=CARTESIAN_POINT('Ctrl Pts',(13.1323548632684,1.83314667576048,-9.94015490134799));
#71442=CARTESIAN_POINT('Ctrl Pts',(12.6361849146757,0.403980496774259,-10.7652843795024));
#71443=CARTESIAN_POINT('Ctrl Pts',(12.8699890291072,9.10811555165335,-5.5695572969706));
#71444=CARTESIAN_POINT('Ctrl Pts',(13.2078467774138,8.14804366490556,-6.12628217974948));
#71445=CARTESIAN_POINT('Ctrl Pts',(13.6453803397493,6.4447365517833,-7.11403939432886));
#71446=CARTESIAN_POINT('Ctrl Pts',(13.7845689781422,3.72407315433307,-8.68667090248933));
#71447=CARTESIAN_POINT('Ctrl Pts',(13.3767756515671,1.71258108335182,-9.84301179383112));
#71448=CARTESIAN_POINT('Ctrl Pts',(12.8699890291072,0.269320331182837,-10.6726380968212));
#71449=CARTESIAN_POINT('Ctrl Pts',(13.1037931435388,9.09521160008097,-5.40661503135002));
#71450=CARTESIAN_POINT('Ctrl Pts',(13.4487286744235,8.12784527924288,-5.96997847813819));
#71451=CARTESIAN_POINT('Ctrl Pts',(13.898714834882,6.40503697970743,-6.97334710224838));
#71452=CARTESIAN_POINT('Ctrl Pts',(14.0431558605194,3.63628981980484,-8.57559554687257));
#71453=CARTESIAN_POINT('Ctrl Pts',(13.6211964398659,1.59201549094316,-9.74586868631426));
#71454=CARTESIAN_POINT('Ctrl Pts',(13.1037931435388,0.134660165591415,-10.57999181414));
#71455=CARTESIAN_POINT('Ctrl Pts',(13.3375972579703,9.08230764850859,-5.24367276572944));
#71456=CARTESIAN_POINT('Ctrl Pts',(13.6896105714332,8.10764689358019,-5.81367477652689));
#71457=CARTESIAN_POINT('Ctrl Pts',(14.1520493300147,6.36533740763156,-6.83265481016789));
#71458=CARTESIAN_POINT('Ctrl Pts',(14.3017427428967,3.54850648527662,-8.46452019125581));
#71459=CARTESIAN_POINT('Ctrl Pts',(13.8656172281646,1.47144989853449,-9.64872557879739));
#71460=CARTESIAN_POINT('Ctrl Pts',(13.3375972579703,-6.34381077890256E-15,
-10.4873455314589));
#71461=CARTESIAN_POINT('Ctrl Pts',(12.6462405439409,0.433014589688015,-10.748521538143));
#71462=CARTESIAN_POINT('Ctrl Pts',(13.1355491140165,1.84924327825183,-9.93086152356657));
#71463=CARTESIAN_POINT('Ctrl Pts',(13.5255929401103,3.81962174635166,-8.7932629846037));
#71464=CARTESIAN_POINT('Ctrl Pts',(13.3924350002713,6.47667086636819,-7.25921495991209));
#71465=CARTESIAN_POINT('Ctrl Pts',(12.9712786667837,8.15112288573676,-6.29246963578454));
#71466=CARTESIAN_POINT('Ctrl Pts',(12.6462397169624,9.09198644037501,-5.74926180924343));
#71467=CARTESIAN_POINT('Origin',(3.,9.30849364905389,-5.37426131403119));
#71468=CARTESIAN_POINT('',(3.,9.09198729810778,-5.74926131403119));
#71469=CARTESIAN_POINT('',(3.,9.525,-4.99926131403119));
#71470=CARTESIAN_POINT('Ctrl Pts',(12.6361849146757,9.525,5.03278481691122));
#71471=CARTESIAN_POINT('Ctrl Pts',(13.1323548632684,9.525,3.3825258606024));
#71472=CARTESIAN_POINT('Ctrl Pts',(13.5261795528199,9.525,1.0975656251991));
#71473=CARTESIAN_POINT('Ctrl Pts',(13.3921464946308,9.525,-1.98832724851366));
#71474=CARTESIAN_POINT('Ctrl Pts',(12.9669648804042,9.525,-3.93261217937201));
#71475=CARTESIAN_POINT('Ctrl Pts',(12.6361849146756,9.525,-5.03278481691123));
#71476=CARTESIAN_POINT('Ctrl Pts',(12.8699890291072,9.3774358828362,5.10308079985062));
#71477=CARTESIAN_POINT('Ctrl Pts',(13.3767756515671,9.3805888048835,3.43836717269219));
#71478=CARTESIAN_POINT('Ctrl Pts',(13.7847648925596,9.38491352314619,1.11803995403544));
#71479=CARTESIAN_POINT('Ctrl Pts',(13.6454811073302,9.38330701946683,-2.02429453530628));
#71480=CARTESIAN_POINT('Ctrl Pts',(13.2078467774138,9.37953783086773,-3.99327171507834));
#71481=CARTESIAN_POINT('Ctrl Pts',(12.8699890291072,9.3774358828362,-5.10308079985063));
#71482=CARTESIAN_POINT('Ctrl Pts',(13.1037931435388,9.2298717656724,5.17337678279002));
#71483=CARTESIAN_POINT('Ctrl Pts',(13.6211964398659,9.236177609767,3.49420848478198));
#71484=CARTESIAN_POINT('Ctrl Pts',(14.0433502322992,9.24482704629237,1.13851428287177));
#71485=CARTESIAN_POINT('Ctrl Pts',(13.8988157200297,9.24161403893366,-2.06026182209891));
#71486=CARTESIAN_POINT('Ctrl Pts',(13.4487286744235,9.23407566173546,-4.05393125078467));
#71487=CARTESIAN_POINT('Ctrl Pts',(13.1037931435388,9.22987176567239,-5.17337678279004));
#71488=CARTESIAN_POINT('Ctrl Pts',(13.3375972579703,9.08230764850859,5.24367276572943));
#71489=CARTESIAN_POINT('Ctrl Pts',(13.8656172281646,9.0917664146505,3.55004979687177));
#71490=CARTESIAN_POINT('Ctrl Pts',(14.3019355720389,9.10474056943856,1.15898861170811));
#71491=CARTESIAN_POINT('Ctrl Pts',(14.1521503327292,9.09992105840049,-2.09622910889154));
#71492=CARTESIAN_POINT('Ctrl Pts',(13.6896105714332,9.0886134926032,-4.114590786491));
#71493=CARTESIAN_POINT('Ctrl Pts',(13.3375972579703,9.08230764850859,-5.24367276572944));
#71494=CARTESIAN_POINT('Ctrl Pts',(12.64623973251,9.525,-4.99926032466067));
#71495=CARTESIAN_POINT('Ctrl Pts',(12.9712796891567,9.525,-3.91284474029011));
#71496=CARTESIAN_POINT('Ctrl Pts',(13.3925359315611,9.525,-1.97936109744437));
#71497=CARTESIAN_POINT('Ctrl Pts',(13.5257901158896,9.525,1.08859947412911));
#71498=CARTESIAN_POINT('Ctrl Pts',(13.1355507160135,9.525,3.36393794605573));
#71499=CARTESIAN_POINT('Ctrl Pts',(12.646240560211,9.525,4.99925912241684));
#71500=CARTESIAN_POINT('Origin',(3.,-1.83880688453542E-15,-10.7485226280624));
#71501=CARTESIAN_POINT('',(3.,-0.433012701892221,-10.7485226280624));
#71502=CARTESIAN_POINT('',(3.,0.433012701892217,-10.7485226280624));
#71503=CARTESIAN_POINT('Origin',(3.,9.30849364905389,5.37426131403119));
#71504=CARTESIAN_POINT('',(3.,9.525,4.99926131403119));
#71505=CARTESIAN_POINT('',(3.,9.09198729810778,5.74926131403119));
#71506=CARTESIAN_POINT('Ctrl Pts',(12.6361849146757,0.403980496774264,10.7652843795024));
#71507=CARTESIAN_POINT('Ctrl Pts',(13.1323548632684,1.83314667576049,9.94015490134798));
#71508=CARTESIAN_POINT('Ctrl Pts',(13.5259820957649,3.8118564888613,8.79774625810608));
#71509=CARTESIAN_POINT('Ctrl Pts',(13.3920458446166,6.48443612385918,7.25473168640934));
#71510=CARTESIAN_POINT('Ctrl Pts',(12.9669648804042,8.16824205056825,6.28258588136077));
#71511=CARTESIAN_POINT('Ctrl Pts',(12.6361849146756,9.12101950322573,5.73249956259117));
#71512=CARTESIAN_POINT('Ctrl Pts',(12.8699890291072,0.269320331182843,10.6726380968212));
#71513=CARTESIAN_POINT('Ctrl Pts',(13.3767756515671,1.71258108335183,9.84301179383112));
#71514=CARTESIAN_POINT('Ctrl Pts',(13.7845689781422,3.72407315433307,8.68667090248932));
#71515=CARTESIAN_POINT('Ctrl Pts',(13.6453803397493,6.44473655178331,7.11403939432886));
#71516=CARTESIAN_POINT('Ctrl Pts',(13.2078467774138,8.14804366490557,6.12628217974947));
#71517=CARTESIAN_POINT('Ctrl Pts',(12.8699890291072,9.10811555165335,5.56955729697059));
#71518=CARTESIAN_POINT('Ctrl Pts',(13.1037931435388,0.134660165591422,10.57999181414));
#71519=CARTESIAN_POINT('Ctrl Pts',(13.6211964398659,1.59201549094317,9.74586868631426));
#71520=CARTESIAN_POINT('Ctrl Pts',(14.0431558605194,3.63628981980485,8.57559554687256));
#71521=CARTESIAN_POINT('Ctrl Pts',(13.898714834882,6.40503697970744,6.97334710224837));
#71522=CARTESIAN_POINT('Ctrl Pts',(13.4487286744235,8.12784527924288,5.96997847813818));
#71523=CARTESIAN_POINT('Ctrl Pts',(13.1037931435388,9.09521160008098,5.40661503135001));
#71524=CARTESIAN_POINT('Ctrl Pts',(13.3375972579703,6.4216470683267E-16,
10.4873455314589));
#71525=CARTESIAN_POINT('Ctrl Pts',(13.8656172281646,1.4714498985345,9.64872557879739));
#71526=CARTESIAN_POINT('Ctrl Pts',(14.3017427428967,3.54850648527663,8.4645201912558));
#71527=CARTESIAN_POINT('Ctrl Pts',(14.1520493300147,6.36533740763157,6.83265481016789));
#71528=CARTESIAN_POINT('Ctrl Pts',(13.6896105714332,8.1076468935802,5.81367477652688));
#71529=CARTESIAN_POINT('Ctrl Pts',(13.3375972579703,9.0823076485086,5.24367276572943));
#71530=CARTESIAN_POINT('Ctrl Pts',(12.6462397169616,9.09198644037732,5.7492618092421));
#71531=CARTESIAN_POINT('Ctrl Pts',(12.9712786667833,8.15112288573813,6.29246963578374));
#71532=CARTESIAN_POINT('Ctrl Pts',(13.3924350002713,6.47667086636881,7.25921495991173));
#71533=CARTESIAN_POINT('Ctrl Pts',(13.5255929401102,3.81962174635229,8.79326298460333));
#71534=CARTESIAN_POINT('Ctrl Pts',(13.1355491140168,1.84924327825312,9.93086152356583));
#71535=CARTESIAN_POINT('Ctrl Pts',(12.6462405439417,0.433014589690331,10.7485215381416));
#71536=CARTESIAN_POINT('Origin',(3.25,2.25625,-9.40720094860847));
#71537=CARTESIAN_POINT('',(3.5,2.38125,-9.62370729955458));
#71538=CARTESIAN_POINT('',(3.,2.13125,-9.19069459766236));
#71539=CARTESIAN_POINT('Origin',(3.,-9.30849364905389,-5.37426131403119));
#71540=CARTESIAN_POINT('',(3.,-9.525,-4.99926131403118));
#71541=CARTESIAN_POINT('',(3.,-9.09198729810778,-5.74926131403119));
#71542=CARTESIAN_POINT('Origin',(3.,2.0122792321331E-15,10.7485226280624));
#71543=CARTESIAN_POINT('',(3.,0.433012701892221,10.7485226280624));
#71544=CARTESIAN_POINT('',(3.,-0.433012701892217,10.7485226280624));
#71545=CARTESIAN_POINT('Origin',(3.25,7.01875,6.65757029159287));
#71546=CARTESIAN_POINT('',(3.5,7.14375,6.87407664253898));
#71547=CARTESIAN_POINT('',(3.,6.89375,6.44106394064676));
#71548=CARTESIAN_POINT('Origin',(3.,-9.30849364905389,5.37426131403119));
#71549=CARTESIAN_POINT('',(3.,-9.09198729810778,5.74926131403119));
#71550=CARTESIAN_POINT('',(3.,-9.525,4.99926131403119));
#71551=CARTESIAN_POINT('Origin',(3.25,-2.25625,9.40720094860847));
#71552=CARTESIAN_POINT('',(3.5,-2.38125,9.62370729955457));
#71553=CARTESIAN_POINT('',(3.,-2.13125,9.19069459766235));
#71554=CARTESIAN_POINT('Origin',(3.,9.525,-5.49926131403119));
#71555=CARTESIAN_POINT('Origin',(3.,0.,0.));
#71556=CARTESIAN_POINT('',(3.,-8.925,-1.09299726823901E-15));
#71557=CARTESIAN_POINT('Origin',(3.,0.,0.));
#71558=CARTESIAN_POINT('Origin',(3.,-2.02039582977095E-15,-10.9985226280624));
#71559=CARTESIAN_POINT('Origin',(3.,-9.525,-5.49926131403119));
#71560=CARTESIAN_POINT('Origin',(3.,9.525,5.49926131403119));
#71561=CARTESIAN_POINT('Origin',(3.,-9.525,5.49926131403119));
#71562=CARTESIAN_POINT('Origin',(3.,6.73465276590316E-16,10.9985226280624));
#71563=CARTESIAN_POINT('Origin',(14.,0.,0.));
#71564=CARTESIAN_POINT('',(13.6,-6.4,-7.83773951454306E-16));
#71565=CARTESIAN_POINT('',(13.6,-7.83773951454306E-16,6.4));
#71566=CARTESIAN_POINT('Origin',(13.6,0.,0.));
#71567=CARTESIAN_POINT('',(14.,-6.8,-8.327598234202E-16));
#71568=CARTESIAN_POINT('Origin',(13.6,0.,0.));
#71569=CARTESIAN_POINT('Origin',(2.,0.,0.));
#71570=CARTESIAN_POINT('',(2.77555756156289E-16,-7.2,-8.81745695386094E-16));
#71571=CARTESIAN_POINT('',(2.,-8.35,-1.02258007728804E-15));
#71572=CARTESIAN_POINT('Origin',(0.,0.,0.));
#71573=CARTESIAN_POINT('Origin',(0.,7.2,0.));
#71574=CARTESIAN_POINT('',(0.,-7.83773951454306E-16,6.4));
#71575=CARTESIAN_POINT('Origin',(0.,0.,0.));
#71576=CARTESIAN_POINT('Origin',(3.,0.,0.));
#71577=CARTESIAN_POINT('',(3.,-7.83773951454306E-16,6.4));
#71612=UNCERTAINTY_MEASURE_WITH_UNIT(LENGTH_MEASURE(0.01),#71629,
'DISTANCE_ACCURACY_VALUE',
'Maximum model space distance between geometric entities at asserted c
onnectivities');
#71613=UNCERTAINTY_MEASURE_WITH_UNIT(LENGTH_MEASURE(0.01),#71629,
'DISTANCE_ACCURACY_VALUE',
'Maximum model space distance between geometric entities at asserted c
onnectivities');
#71627=(
GEOMETRIC_REPRESENTATION_CONTEXT(3)
GLOBAL_UNCERTAINTY_ASSIGNED_CONTEXT((#71612))
GLOBAL_UNIT_ASSIGNED_CONTEXT((#71629,#71631,#71632))
REPRESENTATION_CONTEXT('','3D')
);
#71628=(
GEOMETRIC_REPRESENTATION_CONTEXT(3)
GLOBAL_UNCERTAINTY_ASSIGNED_CONTEXT((#71613))
GLOBAL_UNIT_ASSIGNED_CONTEXT((#71629,#71631,#71632))
REPRESENTATION_CONTEXT('','3D')
);
#71629=(
LENGTH_UNIT()
NAMED_UNIT(*)
SI_UNIT(.MILLI.,.METRE.)
);
#71631=(
NAMED_UNIT(*)
PLANE_ANGLE_UNIT()
SI_UNIT($,.RADIAN.)
);
#71632=(
NAMED_UNIT(*)
SI_UNIT($,.STERADIAN.)
SOLID_ANGLE_UNIT()
);
#71646=SHAPE_DEFINITION_REPRESENTATION(#71660,#71695);
#71660=PRODUCT_DEFINITION_SHAPE('',$,#71710);
#71695=SHAPE_REPRESENTATION('',(#37583),#71627);
#71696=PRODUCT_DEFINITION_CONTEXT('part definition',#71740,'design');
#71710=PRODUCT_DEFINITION('2026-10-25-00-23-50-203',
'03_Lug_Nut_1-2-20_60deg_Cone',#71724,#71696);
#71724=PRODUCT_DEFINITION_FORMATION('',$,#71755);
#71740=APPLICATION_CONTEXT(
'Core Data for Automotive Mechanical Design Process');
#71741=PRODUCT_CONTEXT('part definition',#71740,'mechanical');
#71755=PRODUCT('2026-10-25-00-23-50-203','03_Lug_Nut_1-2-20_60deg_Cone',
$,(#71741));
#71819=COLOUR_RGB('Black',0.12,0.14,0.17);
#71820=FILL_AREA_STYLE_COLOUR('',#71819);
#71821=FILL_AREA_STYLE('',(#71820));
#71822=SURFACE_STYLE_FILL_AREA(#71821);
#71823=SURFACE_SIDE_STYLE('',(#71822));
#71824=SURFACE_STYLE_USAGE(.BOTH.,#71823);
#71825=PRESENTATION_STYLE_ASSIGNMENT((#71824));
ENDSEC;
END-ISO-10303-21;
